ISO-10303-21;
HEADER;
FILE_DESCRIPTION (('STEP AP214'),
    '1' );
FILE_NAME ('5-Cover.step',
    '2026-10-28T16:50:19',
    ( '' ),
    ( '' ),
    'SwSTEP 2.0',
    'SolidWorks 2024',
    '' );
FILE_SCHEMA (( 'AUTOMOTIVE_DESIGN' ));
ENDSEC;

DATA;
#10=CARTESIAN_POINT ( 'NONE',  ( -22.50000000000000000, -7.855833012397050680E-14, 5.000000000000000000 ) ) ;
#13=CARTESIAN_POINT ( 'NONE',  ( 15.00000000000000000, 1.836970198721029589E-15, 11.00000000000000000 ) ) ;
#27=LINE ( 'NONE', #8090, #5201 ) ;
#32=CARTESIAN_POINT ( 'NONE',  ( 3.791949971500756078, 27.16611547376996683, 0.4273392542514659609 ) ) ;
#33=ORIENTED_EDGE ( 'NONE', *, *, #310, .F. ) ;
#82=DIRECTION ( 'NONE',  ( -1.000000000000000000, 0.000000000000000000, 0.000000000000000000 ) ) ;
#94=VECTOR ( 'NONE', #809, 1000.000000000000000 ) ;
#106=VERTEX_POINT ( 'NONE', #5874 ) ;
#114=AXIS2_PLACEMENT_3D ( 'NONE', #1241, #6492, #8505 ) ;
#138=ORIENTED_EDGE ( 'NONE', *, *, #426, .F. ) ;
#139=VECTOR ( 'NONE', #696, 1000.000000000000000 ) ;
#144=EDGE_CURVE ( 'NONE', #410, #1266, #6863, .T. ) ;
#146=ORIENTED_EDGE ( 'NONE', *, *, #4940, .T. ) ;
#155=DIRECTION ( 'NONE',  ( 0.000000000000000000, 0.000000000000000000, -1.000000000000000000 ) ) ;
#164=ORIENTED_EDGE ( 'NONE', *, *, #7741, .T. ) ;
#166=ORIENTED_EDGE ( 'NONE', *, *, #8588, .F. ) ;
#201=FACE_BOUND ( 'NONE', #3357, .T. ) ;
#206=CIRCLE ( 'NONE', #2661, 6.000000000000000000 ) ;
#208=DIRECTION ( 'NONE',  ( 1.000000000000000000, 0.000000000000000000, 0.000000000000000000 ) ) ;
#223=CARTESIAN_POINT ( 'NONE',  ( 28.00000000000000711, 3.551475717527324030E-15, 10.00000000000000000 ) ) ;
#227=CARTESIAN_POINT ( 'NONE',  ( -22.50000000000000000, -7.855833012397050680E-14, 10.00000000000000000 ) ) ;
#230=MECHANICAL_DESIGN_GEOMETRIC_PRESENTATION_REPRESENTATION('',(#5131),#1330);
#247=DIRECTION ( 'NONE',  ( 0.000000000000000000, 0.000000000000000000, -1.000000000000000000 ) ) ;
#249=LINE ( 'NONE', #1829, #3671 ) ;
#252=DIRECTION ( 'NONE',  ( 0.000000000000000000, 0.000000000000000000, -1.000000000000000000 ) ) ;
#310=EDGE_CURVE ( 'NONE', #883, #5200, #6979, .T. ) ;
#339=DIRECTION ( 'NONE',  ( -1.000000000000000000, 0.000000000000000000, 0.000000000000000000 ) ) ;
#358=DIRECTION ( 'NONE',  ( -1.000000000000000000, 0.000000000000000000, 0.000000000000000000 ) ) ;
#364=ADVANCED_FACE ( 'NONE', ( #3272, #6212 ), #5492, .T. ) ;
#366=DIRECTION ( 'NONE',  ( -1.000000000000000000, 0.000000000000000000, 0.000000000000000000 ) ) ;
#375=CARTESIAN_POINT ( 'NONE',  ( 6.000000000000157208, -22.50000000000000355, 5.000000000000000000 ) ) ;
#392=CARTESIAN_POINT ( 'NONE',  ( 0.000000000000000000, 0.000000000000000000, 0.000000000000000000 ) ) ;
#406=CARTESIAN_POINT ( 'NONE',  ( -6.000000000000000888, 22.50000000000000355, 5.000000000000000000 ) ) ;
#410=VERTEX_POINT ( 'NONE', #8203 ) ;
#413=DIRECTION ( 'NONE',  ( -1.000000000000000000, 0.000000000000000000, -0.000000000000000000 ) ) ;
#426=EDGE_CURVE ( 'NONE', #7367, #6082, #2257, .T. ) ;
#429=SHAPE_DEFINITION_REPRESENTATION ( #1557, #6964 ) ;
#442=AXIS2_PLACEMENT_3D ( 'NONE', #1442, #3660, #4332 ) ;
#456=CARTESIAN_POINT ( 'NONE',  ( -28.50000000000000000, -7.855833012397050680E-14, 5.000000000000000000 ) ) ;
#468=CARTESIAN_POINT ( 'NONE',  ( -5.999999999999842792, -22.50000000000000355, 0.000000000000000000 ) ) ;
#471=ORIENTED_EDGE ( 'NONE', *, *, #2053, .F. ) ;
#480=ORIENTED_EDGE ( 'NONE', *, *, #2220, .T. ) ;
#491=ORIENTED_EDGE ( 'NONE', *, *, #4676, .F. ) ;
#503=EDGE_LOOP ( 'NONE', ( #6940, #1509 ) ) ;
#504=CARTESIAN_POINT ( 'NONE',  ( -4.333301281932778082, 26.64999999999997371, 0.000000000000000000 ) ) ;
#510=CIRCLE ( 'NONE', #7729, 2.999999999999999112 ) ;
#515=ORIENTED_EDGE ( 'NONE', *, *, #5543, .T. ) ;
#518=VECTOR ( 'NONE', #1188, 1000.000000000000000 ) ;
#524=ORIENTED_EDGE ( 'NONE', *, *, #7444, .F. ) ;
#547=DIRECTION ( 'NONE',  ( -0.000000000000000000, -0.000000000000000000, -1.000000000000000000 ) ) ;
#558=CONICAL_SURFACE ( 'NONE', #5167, 30.00000000000000000, 0.7853981633974428389 ) ;
#565=CARTESIAN_POINT ( 'NONE',  ( -25.50000000000000000, -7.855833012397050680E-14, 15.00000000000000000 ) ) ;
#583=CARTESIAN_POINT ( 'NONE',  ( 0.000000000000000000, 0.000000000000000000, 10.00000000000000000 ) ) ;
#585=FACE_OUTER_BOUND ( 'NONE', #9353, .T. ) ;
#592=FACE_OUTER_BOUND ( 'NONE', #5726, .T. ) ;
#595=CARTESIAN_POINT ( 'NONE',  ( -15.00000000000000000, 0.000000000000000000, 20.00000000000000000 ) ) ;
#596=ADVANCED_FACE ( 'NONE', ( #3209, #947, #3160, #6099, #7678, #2538 ), #2588, .T. ) ;
#612=CYLINDRICAL_SURFACE ( 'NONE', #5951, 6.000000000000000000 ) ;
#620=DIRECTION ( 'NONE',  ( 0.000000000000000000, 0.000000000000000000, 1.000000000000000000 ) ) ;
#621=CIRCLE ( 'NONE', #9367, 2.999999999999999556 ) ;
#625=ORIENTED_EDGE ( 'NONE', *, *, #1373, .T. ) ;
#631=CARTESIAN_POINT ( 'NONE',  ( 30.00000000000000000, 3.673940397442059178E-15, 8.000000000000005329 ) ) ;
#632=CARTESIAN_POINT ( 'NONE',  ( 3.000000000000000000, 22.50000000000000355, 5.000000000000000000 ) ) ;
#640=EDGE_CURVE ( 'NONE', #410, #2498, #1672, .T. ) ;
#641=CARTESIAN_POINT ( 'NONE',  ( 0.000000000000000000, 0.000000000000000000, 3.000000000000052847 ) ) ;
#648=ORIENTED_EDGE ( 'NONE', *, *, #5543, .F. ) ;
#656=AXIS2_PLACEMENT_3D ( 'NONE', #6323, #2670, #8522 ) ;
#659=FACE_OUTER_BOUND ( 'NONE', #8233, .T. ) ;
#667=DIRECTION ( 'NONE',  ( 0.000000000000000000, 0.000000000000000000, 1.000000000000000000 ) ) ;
#671=ORIENTED_EDGE ( 'NONE', *, *, #5315, .T. ) ;
#689=CARTESIAN_POINT ( 'NONE',  ( 2.081312099201997334, -28.14194242914269140, 1.216216932313274102 ) ) ;
#693=CARTESIAN_POINT ( 'NONE',  ( 4.333301281932778082, 26.64999999999997371, 0.000000000000000000 ) ) ;
#695=CARTESIAN_POINT ( 'NONE',  ( -28.40898306695984843, -1.062480114423898225, 1.428075945201411789 ) ) ;
#696=DIRECTION ( 'NONE',  ( -0.000000000000000000, -0.000000000000000000, -1.000000000000000000 ) ) ;
#698=CYLINDRICAL_SURFACE ( 'NONE', #2313, 3.000000000000000000 ) ;
#714=ADVANCED_FACE ( 'NONE', ( #4259 ), #9391, .T. ) ;
#717=EDGE_LOOP ( 'NONE', ( #6670, #5208 ) ) ;
#720=VERTEX_POINT ( 'NONE', #8674 ) ;
#740=EDGE_LOOP ( 'NONE', ( #5086, #9445 ) ) ;
#744=CARTESIAN_POINT ( 'NONE',  ( -25.50000000000000000, -7.855833012397050680E-14, 10.00000000000000000 ) ) ;
#754=VERTEX_POINT ( 'NONE', #6293 ) ;
#762=ORIENTED_EDGE ( 'NONE', *, *, #5774, .F. ) ;
#773=AXIS2_PLACEMENT_3D ( 'NONE', #2389, #939, #3871 ) ;
#777=VERTEX_POINT ( 'NONE', #5071 ) ;
#781=DIRECTION ( 'NONE',  ( 1.000000000000000000, 0.000000000000000000, 0.000000000000000000 ) ) ;
#809=DIRECTION ( 'NONE',  ( -0.000000000000000000, -0.000000000000000000, -1.000000000000000000 ) ) ;
#817=ORIENTED_EDGE ( 'NONE', *, *, #7545, .F. ) ;
#820=CARTESIAN_POINT ( 'NONE',  ( 1.571166602479410136E-13, -22.50000000000000355, 0.000000000000000000 ) ) ;
#828=AXIS2_PLACEMENT_3D ( 'NONE', #5412, #7671, #8527 ) ;
#843=CYLINDRICAL_SURFACE ( 'NONE', #2052, 2.999999999999999556 ) ;
#883=VERTEX_POINT ( 'NONE', #744 ) ;
#890=CARTESIAN_POINT ( 'NONE',  ( 30.00000000000000000, 0.000000000000000000, 3.000000000000052847 ) ) ;
#901=ORIENTED_EDGE ( 'NONE', *, *, #8588, .T. ) ;
#907=EDGE_CURVE ( 'NONE', #6587, #7179, #5822, .T. ) ;
#914=CARTESIAN_POINT ( 'NONE',  ( 0.000000000000000000, 0.000000000000000000, 3.000000000000052847 ) ) ;
#920=CARTESIAN_POINT ( 'NONE',  ( 0.4367635713303894551, -28.48785780768278286, 1.490418226835889426 ) ) ;
#926=DIRECTION ( 'NONE',  ( -0.000000000000000000, -0.000000000000000000, -1.000000000000000000 ) ) ;
#939=DIRECTION ( 'NONE',  ( 0.000000000000000000, 0.000000000000000000, -1.000000000000000000 ) ) ;
#947=FACE_OUTER_BOUND ( 'NONE', #6280, .T. ) ;
#957=AXIS2_PLACEMENT_3D ( 'NONE', #5381, #8341, #1764 ) ;
#966=DIRECTION ( 'NONE',  ( -1.000000000000000000, 0.000000000000000000, 0.000000000000000000 ) ) ;
#1002=PRODUCT_DEFINITION_FORMATION_WITH_SPECIFIED_SOURCE ( 'ANY', '', #9448, .NOT_KNOWN. ) ;
#1022=AXIS2_PLACEMENT_3D ( 'NONE', #7357, #1546, #3901 ) ;
#1028=CIRCLE ( 'NONE', #4104, 15.00000000000000000 ) ;
#1039=FACE_OUTER_BOUND ( 'NONE', #3301, .T. ) ;
#1047=ORIENTED_EDGE ( 'NONE', *, *, #1240, .F. ) ;
#1081=CARTESIAN_POINT ( 'NONE',  ( 27.16400976452047189, 3.794195651236313083, 0.4256031388450388087 ) ) ;
#1084=DIRECTION ( 'NONE',  ( 0.000000000000000000, 0.000000000000000000, -1.000000000000000000 ) ) ;
#1107=VERTEX_POINT ( 'NONE', #3705 ) ;
#1123=EDGE_CURVE ( 'NONE', #754, #5200, #1208, .T. ) ;
#1130=ORIENTED_EDGE ( 'NONE', *, *, #3044, .T. ) ;
#1135=CARTESIAN_POINT ( 'NONE',  ( 26.65000000000001634, -4.333301281932499194, 0.000000000000000000 ) ) ;
#1169=VECTOR ( 'NONE', #7368, 1000.000000000000000 ) ;
#1170=DIRECTION ( 'NONE',  ( 0.000000000000000000, 0.000000000000000000, -1.000000000000000000 ) ) ;
#1177=AXIS2_PLACEMENT_3D ( 'NONE', #1549, #7407, #4527 ) ;
#1180=DIRECTION ( 'NONE',  ( -1.000000000000000000, 0.000000000000000000, 0.000000000000000000 ) ) ;
#1186=VECTOR ( 'NONE', #1880, 1000.000000000000000 ) ;
#1188=DIRECTION ( 'NONE',  ( -0.000000000000000000, -0.000000000000000000, -1.000000000000000000 ) ) ;
#1205=FACE_OUTER_BOUND ( 'NONE', #3087, .T. ) ;
#1208=CIRCLE ( 'NONE', #1360, 2.999999999999999112 ) ;
#1217=CARTESIAN_POINT ( 'NONE',  ( 28.44339478698105594, 0.8493939025105605722, 1.455282208020844514 ) ) ;
#1237=ADVANCED_FACE ( 'NONE', ( #7593 ), #8272, .T. ) ;
#1240=EDGE_CURVE ( 'NONE', #4833, #3516, #249, .T. ) ;
#1241=CARTESIAN_POINT ( 'NONE',  ( 0.000000000000000000, 0.000000000000000000, 20.00000000000000000 ) ) ;
#1243=ORIENTED_EDGE ( 'NONE', *, *, #4505, .T. ) ;
#1248=LINE ( 'NONE', #3457, #2096 ) ;
#1257=EDGE_LOOP ( 'NONE', ( #1047, #1658, #1794, #3252 ) ) ;
#1258=DIRECTION ( 'NONE',  ( 0.000000000000000000, 0.000000000000000000, -1.000000000000000000 ) ) ;
#1259=CARTESIAN_POINT ( 'NONE',  ( -28.13653351783515788, 2.066994717595188824, 1.211640400093613179 ) ) ;
#1260=FACE_OUTER_BOUND ( 'NONE', #5174, .T. ) ;
#1266=VERTEX_POINT ( 'NONE', #6885 ) ;
#1270=FACE_OUTER_BOUND ( 'NONE', #7923, .T. ) ;
#1284=CARTESIAN_POINT ( 'NONE',  ( 15.00000000000000000, 1.836970198721029589E-15, 20.00000000000000000 ) ) ;
#1296=DIRECTION ( 'NONE',  ( -0.000000000000000000, -0.000000000000000000, -1.000000000000000000 ) ) ;
#1299=CYLINDRICAL_SURFACE ( 'NONE', #4634, 2.999999999999999112 ) ;
#1306=CARTESIAN_POINT ( 'NONE',  ( -26.64999999999998792, 4.333301281932682159, 0.000000000000000000 ) ) ;
#1320=CARTESIAN_POINT ( 'NONE',  ( -28.00000000000000711, 0.000000000000000000, 10.00000000000000000 ) ) ;
#1330=( GEOMETRIC_REPRESENTATION_CONTEXT ( 3 ) GLOBAL_UNCERTAINTY_ASSIGNED_CONTEXT ( ( #7388 ) ) GLOBAL_UNIT_ASSIGNED_CONTEXT ( ( #7074, #8516, #1935 ) ) REPRESENTATION_CONTEXT ( 'NONE', 'WORKASPACE' ) );
#1339=AXIS2_PLACEMENT_3D ( 'NONE', #2961, #2869, #5850 ) ;
#1346=CARTESIAN_POINT ( 'NONE',  ( 28.26575725008336093, -1.673027373761835079, 1.314514334795901185 ) ) ;
#1347=DIRECTION ( 'NONE',  ( -0.000000000000000000, -0.000000000000000000, -1.000000000000000000 ) ) ;
#1349=CARTESIAN_POINT ( 'NONE',  ( 22.50000000000000355, 2.356749903719115078E-13, 15.00000000000000000 ) ) ;
#1351=CIRCLE ( 'NONE', #6739, 28.00000000000000711 ) ;
#1359=EDGE_CURVE ( 'NONE', #2727, #6154, #4177, .T. ) ;
#1360=AXIS2_PLACEMENT_3D ( 'NONE', #8939, #7304, #9469 ) ;
#1364=CARTESIAN_POINT ( 'NONE',  ( -4.333301281932591564, -26.65000000000000213, 0.000000000000000000 ) ) ;
#1373=EDGE_CURVE ( 'NONE', #4405, #2727, #5170, .T. ) ;
#1382=LINE ( 'NONE', #3494, #1802 ) ;
#1387=ORIENTED_EDGE ( 'NONE', *, *, #8390, .F. ) ;
#1401=DIRECTION ( 'NONE',  ( -1.000000000000000000, 0.000000000000000000, 0.000000000000000000 ) ) ;
#1407=CARTESIAN_POINT ( 'NONE',  ( -0.4129292217235346896, -28.50085334706576035, 1.500673695285822395 ) ) ;
#1408=ORIENTED_EDGE ( 'NONE', *, *, #4238, .F. ) ;
#1414=CARTESIAN_POINT ( 'NONE',  ( 16.50000000000000000, 2.356749903719115078E-13, 5.000000000000000000 ) ) ;
#1433=ORIENTED_EDGE ( 'NONE', *, *, #7153, .F. ) ;
#1439=CARTESIAN_POINT ( 'NONE',  ( 27.16490240584779059, -3.793344078502343564, 0.4263419363949833008 ) ) ;
#1442=CARTESIAN_POINT ( 'NONE',  ( 0.000000000000000000, 22.50000000000000355, 0.000000000000000000 ) ) ;
#1445=AXIS2_PLACEMENT_3D ( 'NONE', #1467, #4496, #8107 ) ;
#1462=FACE_OUTER_BOUND ( 'NONE', #8040, .T. ) ;
#1464=DIRECTION ( 'NONE',  ( 1.000000000000000000, 0.000000000000000000, 0.000000000000000000 ) ) ;
#1467=CARTESIAN_POINT ( 'NONE',  ( -22.50000000000000000, -7.855833012397050680E-14, 5.000000000000000000 ) ) ;
#1476=AXIS2_PLACEMENT_3D ( 'NONE', #9053, #6229, #358 ) ;
#1480=ORIENTED_EDGE ( 'NONE', *, *, #1824, .F. ) ;
#1486=AXIS2_PLACEMENT_3D ( 'NONE', #8756, #6607, #5205 ) ;
#1489=AXIS2_PLACEMENT_3D ( 'NONE', #7918, #2918, #5041 ) ;
#1492=CARTESIAN_POINT ( 'NONE',  ( 4.333301281932962823, -26.64999999999994529, 0.000000000000000000 ) ) ;
#1499=CIRCLE ( 'NONE', #3349, 6.000000000000001776 ) ;
#1500=VERTEX_POINT ( 'NONE', #8165 ) ;
#1504=CIRCLE ( 'NONE', #7650, 6.000000000000001776 ) ;
#1506=ORIENTED_EDGE ( 'NONE', *, *, #144, .T. ) ;
#1509=ORIENTED_EDGE ( 'NONE', *, *, #1123, .F. ) ;
#1513=AXIS2_PLACEMENT_3D ( 'NONE', #2817, #3389, #5754 ) ;
#1531=ORIENTED_EDGE ( 'NONE', *, *, #5481, .F. ) ;
#1535=EDGE_CURVE ( 'NONE', #1500, #6154, #1028, .T. ) ;
#1546=DIRECTION ( 'NONE',  ( 0.000000000000000000, 0.000000000000000000, -1.000000000000000000 ) ) ;
#1549=CARTESIAN_POINT ( 'NONE',  ( 0.000000000000000000, 22.50000000000000355, 5.000000000000000000 ) ) ;
#1557=PRODUCT_DEFINITION_SHAPE ( 'NONE', 'NONE',  #8051 ) ;
#1563=DIRECTION ( 'NONE',  ( -0.000000000000000000, -0.000000000000000000, -1.000000000000000000 ) ) ;
#1565=DIRECTION ( 'NONE',  ( 0.000000000000000000, 0.000000000000000000, 1.000000000000000000 ) ) ;
#1582=CARTESIAN_POINT ( 'NONE',  ( 0.000000000000000000, 22.50000000000000355, 5.000000000000000000 ) ) ;
#1599=FACE_OUTER_BOUND ( 'NONE', #7856, .T. ) ;
#1606=( NAMED_UNIT ( * ) PLANE_ANGLE_UNIT ( ) SI_UNIT ( $, .RADIAN. ) );
#1614=AXIS2_PLACEMENT_3D ( 'NONE', #6760, #5504, #4539 ) ;
#1616=DIRECTION ( 'NONE',  ( 1.000000000000000000, 0.000000000000000000, 0.000000000000000000 ) ) ;
#1618=ORIENTED_EDGE ( 'NONE', *, *, #7580, .T. ) ;
#1631=ORIENTED_EDGE ( 'NONE', *, *, #2262, .F. ) ;
#1640=FACE_OUTER_BOUND ( 'NONE', #7306, .T. ) ;
#1657=ORIENTED_EDGE ( 'NONE', *, *, #7827, .F. ) ;
#1658=ORIENTED_EDGE ( 'NONE', *, *, #7044, .T. ) ;
#1659=ORIENTED_EDGE ( 'NONE', *, *, #1359, .T. ) ;
#1672=CIRCLE ( 'NONE', #2752, 26.99999999999997868 ) ;
#1677=VERTEX_POINT ( 'NONE', #8306 ) ;
#1686=DIRECTION ( 'NONE',  ( -0.000000000000000000, -0.000000000000000000, 1.000000000000000000 ) ) ;
#1701=VERTEX_POINT ( 'NONE', #375 ) ;
#1708=CARTESIAN_POINT ( 'NONE',  ( -6.000000000000000888, 22.50000000000000355, 5.000000000000000000 ) ) ;
#1747=( LENGTH_UNIT ( ) NAMED_UNIT ( * ) SI_UNIT ( .MILLI., .METRE. ) );
#1764=DIRECTION ( 'NONE',  ( 1.000000000000000000, 0.000000000000000000, -0.000000000000000000 ) ) ;
#1774=FACE_OUTER_BOUND ( 'NONE', #7836, .T. ) ;
#1776=CARTESIAN_POINT ( 'NONE',  ( 3.000000000000156763, -22.50000000000000355, 5.000000000000000000 ) ) ;
#1777=AXIS2_PLACEMENT_3D ( 'NONE', #914, #1686, #7772 ) ;
#1784=AXIS2_PLACEMENT_3D ( 'NONE', #3868, #8288, #2626 ) ;
#1793=ORIENTED_EDGE ( 'NONE', *, *, #2121, .F. ) ;
#1794=ORIENTED_EDGE ( 'NONE', *, *, #7444, .T. ) ;
#1802=VECTOR ( 'NONE', #2059, 1000.000000000000000 ) ;
#1803=CARTESIAN_POINT ( 'NONE',  ( 27.81412668510617436, 2.815004828058581765, 0.9535900900804922253 ) ) ;
#1817=CIRCLE ( 'NONE', #7184, 2.999999999999999112 ) ;
#1824=EDGE_CURVE ( 'NONE', #1107, #1266, #7910, .T. ) ;
#1829=CARTESIAN_POINT ( 'NONE',  ( 30.00000000000000000, 3.673940397442059178E-15, 10.00000000000000000 ) ) ;
#1839=ADVANCED_FACE ( 'NONE', ( #659 ), #8820, .F. ) ;
#1844=ORIENTED_EDGE ( 'NONE', *, *, #5942, .T. ) ;
#1851=CYLINDRICAL_SURFACE ( 'NONE', #1476, 6.000000000000000888 ) ;
#1857=VERTEX_POINT ( 'NONE', #7377 ) ;
#1868=ORIENTED_EDGE ( 'NONE', *, *, #7827, .T. ) ;
#1880=DIRECTION ( 'NONE',  ( -0.000000000000000000, -0.000000000000000000, -1.000000000000000000 ) ) ;
#1898=CARTESIAN_POINT ( 'NONE',  ( 28.40898306695985198, 1.062480114424067201, 1.428075945201422670 ) ) ;
#1899=CARTESIAN_POINT ( 'NONE',  ( 0.000000000000000000, 0.000000000000000000, 0.000000000000000000 ) ) ;
#1902=ADVANCED_FACE ( 'NONE', ( #5122 ), #612, .F. ) ;
#1935=( NAMED_UNIT ( * ) SI_UNIT ( $, .STERADIAN. ) SOLID_ANGLE_UNIT ( ) );
#1951=CARTESIAN_POINT ( 'NONE',  ( -30.00000000000000000, 0.000000000000000000, 8.000000000000005329 ) ) ;
#1969=VERTEX_POINT ( 'NONE', #5414 ) ;
#1983=CARTESIAN_POINT ( 'NONE',  ( -16.49999999999999645, -7.782354204448209592E-14, 5.000000000000000000 ) ) ;
#1989=EDGE_LOOP ( 'NONE', ( #6194, #480, #5703, #4934, #7292, #8842, #7858, #5388, #2654, #6980, #6791, #7059, #8507, #1433 ) ) ;
#1991=CARTESIAN_POINT ( 'NONE',  ( -28.50000000000000000, -7.855833971761515132E-14, 1.500000000000037748 ) ) ;
#1997=ORIENTED_EDGE ( 'NONE', *, *, #9457, .T. ) ;
#2000=CARTESIAN_POINT ( 'NONE',  ( 0.000000000000000000, 0.000000000000000000, 0.000000000000000000 ) ) ;
#2009=ORIENTED_EDGE ( 'NONE', *, *, #7704, .T. ) ;
#2021=ORIENTED_EDGE ( 'NONE', *, *, #7626, .F. ) ;
#2023=ADVANCED_FACE ( 'NONE', ( #1039 ), #843, .F. ) ;
#2028=ADVANCED_FACE ( 'NONE', ( #6190 ), #7424, .F. ) ;
#2034=ORIENTED_EDGE ( 'NONE', *, *, #7580, .F. ) ;
#2050=LINE ( 'NONE', #1320, #7300 ) ;
#2052=AXIS2_PLACEMENT_3D ( 'NONE', #6769, #8336, #3107 ) ;
#2053=EDGE_CURVE ( 'NONE', #5050, #883, #4811, .T. ) ;
#2059=DIRECTION ( 'NONE',  ( -0.000000000000000000, -0.000000000000000000, -1.000000000000000000 ) ) ;
#2062=DIRECTION ( 'NONE',  ( 0.000000000000000000, 0.000000000000000000, 1.000000000000000000 ) ) ;
#2080=CARTESIAN_POINT ( 'NONE',  ( -28.32042821893188744, 1.471975546721317141, 1.357900206176153146 ) ) ;
#2083=CARTESIAN_POINT ( 'NONE',  ( 2.819222834329444538, -27.81181297095828597, 0.9517275379012076764 ) ) ;
#2091=AXIS2_PLACEMENT_3D ( 'NONE', #6944, #4060, #9138 ) ;
#2096=VECTOR ( 'NONE', #1347, 1000.000000000000000 ) ;
#2107=DIRECTION ( 'NONE',  ( -0.000000000000000000, -0.000000000000000000, -1.000000000000000000 ) ) ;
#2116=CARTESIAN_POINT ( 'NONE',  ( 28.50000000000000355, 2.364097784513999692E-13, 5.000000000000000000 ) ) ;
#2121=EDGE_CURVE ( 'NONE', #4182, #5535, #7809, .T. ) ;
#2133=CARTESIAN_POINT ( 'NONE',  ( 22.50000000000000355, 2.356749903719115078E-13, 5.000000000000000000 ) ) ;
#2140=ADVANCED_FACE ( 'NONE', ( #9239 ), #2582, .F. ) ;
#2141=CARTESIAN_POINT ( 'NONE',  ( -28.27439555746436284, -1.684082973785163029, 1.321420441384538069 ) ) ;
#2162=CARTESIAN_POINT ( 'NONE',  ( 28.45342843414351464, -0.8561988828940789720, 1.463295953604768940 ) ) ;
#2165=DIRECTION ( 'NONE',  ( 0.7071067811865469066, 8.659560562354925463E-17, -0.7071067811865481278 ) ) ;
#2173=FACE_BOUND ( 'NONE', #2669, .T. ) ;
#2185=B_SPLINE_CURVE_WITH_KNOTS ( 'NONE', 3,
 ( #3523, #4576, #7996, #5249, #2083, #689, #4345, #2859, #5748, #920, #6020, #1407, #5297, #2811, #3852, #9385, #8176, #5791, #7952, #6788, #6562, #1364 ),
 .UNSPECIFIED., .F., .F.,
 ( 4, 2, 2, 2, 2, 2, 2, 2, 2, 2, 4 ),
 ( 1.026960276838673439E-18, 0.001276335940410830774, 0.002552671880821660248, 0.003829007821232489721, 0.004467175791437904241, 0.005105343761643319628, 0.006381679702054149535, 0.007019847672259564055, 0.007658015642464980309, 0.008934351582875806747, 0.01021068752328663232 ),
 .UNSPECIFIED. ) ;
#2189=CIRCLE ( 'NONE', #3415, 30.00000000000000000 ) ;
#2198=VECTOR ( 'NONE', #2107, 1000.000000000000000 ) ;
#2204=ORIENTED_EDGE ( 'NONE', *, *, #5774, .T. ) ;
#2219=ORIENTED_EDGE ( 'NONE', *, *, #6195, .F. ) ;
#2220=EDGE_CURVE ( 'NONE', #106, #6587, #6199, .T. ) ;
#2229=DIRECTION ( 'NONE',  ( 0.7071067811865435759, 0.000000000000000000, 0.7071067811865513475 ) ) ;
#2240=EDGE_LOOP ( 'NONE', ( #7413, #1997 ) ) ;
#2257=CIRCLE ( 'NONE', #5026, 3.000000000000000000 ) ;
#2262=EDGE_CURVE ( 'NONE', #2573, #4625, #2516, .T. ) ;
#2285=CYLINDRICAL_SURFACE ( 'NONE', #8111, 6.000000000000000000 ) ;
#2290=CARTESIAN_POINT ( 'NONE',  ( 0.000000000000000000, 0.000000000000000000, 11.00000000000000000 ) ) ;
#2300=EDGE_CURVE ( 'NONE', #6171, #106, #2185, .T. ) ;
#2306=EDGE_CURVE ( 'NONE', #7179, #6408, #8941, .T. ) ;
#2309=EDGE_LOOP ( 'NONE', ( #2034, #7755, #8579, #1130 ) ) ;
#2313=AXIS2_PLACEMENT_3D ( 'NONE', #9293, #8585, #4264 ) ;
#2320=DIRECTION ( 'NONE',  ( -0.7071067811865435759, 8.659560562354886020E-17, 0.7071067811865513475 ) ) ;
#2339=CARTESIAN_POINT ( 'NONE',  ( 0.000000000000000000, 0.000000000000000000, 10.00000000000000000 ) ) ;
#2347=EDGE_CURVE ( 'NONE', #4182, #1107, #2813, .T. ) ;
#2357=EDGE_LOOP ( 'NONE', ( #7252, #1618, #8178, #33 ) ) ;
#2366=CARTESIAN_POINT ( 'NONE',  ( 28.00000000000000711, 3.429011037612589670E-15, 10.00000000000000000 ) ) ;
#2369=ADVANCED_FACE ( 'NONE', ( #6264 ), #7595, .F. ) ;
#2380=ORIENTED_EDGE ( 'NONE', *, *, #3656, .F. ) ;
#2385=ORIENTED_EDGE ( 'NONE', *, *, #640, .F. ) ;
#2389=CARTESIAN_POINT ( 'NONE',  ( 0.000000000000000000, 22.50000000000000355, 0.000000000000000000 ) ) ;
#2401=CARTESIAN_POINT ( 'NONE',  ( 1.571166602479410136E-13, -22.50000000000000355, 5.000000000000000000 ) ) ;
#2410=DIRECTION ( 'NONE',  ( -0.000000000000000000, -0.000000000000000000, -1.000000000000000000 ) ) ;
#2415=CARTESIAN_POINT ( 'NONE',  ( 0.000000000000000000, 22.50000000000000355, 5.000000000000000000 ) ) ;
#2445=DIRECTION ( 'NONE',  ( 1.000000000000000000, 0.000000000000000000, 0.000000000000000000 ) ) ;
#2460=ORIENTED_EDGE ( 'NONE', *, *, #2544, .F. ) ;
#2463=DIRECTION ( 'NONE',  ( 0.000000000000000000, 0.000000000000000000, -1.000000000000000000 ) ) ;
#2469=EDGE_CURVE ( 'NONE', #5629, #5930, #510, .T. ) ;
#2480=APPLICATION_CONTEXT ( 'automotive_design' ) ;
#2485=CARTESIAN_POINT ( 'NONE',  ( 22.50000000000000355, 2.356749903719115078E-13, 5.000000000000000000 ) ) ;
#2487=CARTESIAN_POINT ( 'NONE',  ( -22.50000000000000000, -7.855833012397050680E-14, 10.00000000000000000 ) ) ;
#2497=DIRECTION ( 'NONE',  ( 0.000000000000000000, 0.000000000000000000, -1.000000000000000000 ) ) ;
#2498=VERTEX_POINT ( 'NONE', #7784 ) ;
#2516=CIRCLE ( 'NONE', #5273, 16.00000000000000000 ) ;
#2538=FACE_BOUND ( 'NONE', #9289, .T. ) ;
#2544=EDGE_CURVE ( 'NONE', #1969, #6082, #9407, .T. ) ;
#2552=CYLINDRICAL_SURFACE ( 'NONE', #6568, 3.000000000000000000 ) ;
#2554=AXIS2_PLACEMENT_3D ( 'NONE', #7004, #2463, #413 ) ;
#2558=DIRECTION ( 'NONE',  ( 1.000000000000000000, 0.000000000000000000, -0.000000000000000000 ) ) ;
#2560=ORIENTED_EDGE ( 'NONE', *, *, #5065, .T. ) ;
#2563=ADVANCED_FACE ( 'NONE', ( #6395 ), #8594, .F. ) ;
#2573=VERTEX_POINT ( 'NONE', #8641 ) ;
#2576=DIRECTION ( 'NONE',  ( -1.000000000000000000, 0.000000000000000000, 0.000000000000000000 ) ) ;
#2582=CYLINDRICAL_SURFACE ( 'NONE', #4355, 6.000000000000001776 ) ;
#2588=PLANE ( 'NONE',  #957 ) ;
#2605=ADVANCED_FACE ( 'NONE', ( #8164 ), #5857, .F. ) ;
#2617=DIRECTION ( 'NONE',  ( -0.000000000000000000, -0.000000000000000000, -1.000000000000000000 ) ) ;
#2620=ORIENTED_EDGE ( 'NONE', *, *, #2901, .T. ) ;
#2626=DIRECTION ( 'NONE',  ( -1.000000000000000000, 0.000000000000000000, -0.000000000000000000 ) ) ;
#2629=CARTESIAN_POINT ( 'NONE',  ( 26.91700667250950829, 4.077589154199230848, 0.2225055604246540530 ) ) ;
#2651=CARTESIAN_POINT ( 'NONE',  ( -25.50000000000000000, -7.855833012397050680E-14, 5.000000000000000000 ) ) ;
#2654=ORIENTED_EDGE ( 'NONE', *, *, #640, .T. ) ;
#2661=AXIS2_PLACEMENT_3D ( 'NONE', #3517, #1258, #6283 ) ;
#2667=ORIENTED_EDGE ( 'NONE', *, *, #8210, .T. ) ;
#2669=EDGE_LOOP ( 'NONE', ( #138, #6352 ) ) ;
#2670=DIRECTION ( 'NONE',  ( 1.224646799147353207E-16, 1.000000000000000000, -0.000000000000000000 ) ) ;
#2671=AXIS2_PLACEMENT_3D ( 'NONE', #6209, #7549, #2558 ) ;
#2687=DIRECTION ( 'NONE',  ( -0.000000000000000000, -0.000000000000000000, -1.000000000000000000 ) ) ;
#2693=CARTESIAN_POINT ( 'NONE',  ( 22.50000000000000355, 2.356749903719115078E-13, 10.00000000000000000 ) ) ;
#2713=CARTESIAN_POINT ( 'NONE',  ( -28.45342843414351108, 0.8561988828942436180, 1.463295953604768496 ) ) ;
#2721=DIRECTION ( 'NONE',  ( -0.000000000000000000, -0.000000000000000000, -1.000000000000000000 ) ) ;
#2727=VERTEX_POINT ( 'NONE', #3838 ) ;
#2736=B_SPLINE_CURVE_WITH_KNOTS ( 'NONE', 3,
 ( #8484, #2629, #1081, #5559, #1803, #8334, #3201, #1898, #1217, #6907, #8441, #4691 ),
 .UNSPECIFIED., .F., .F.,
 ( 4, 2, 2, 2, 2, 4 ),
 ( 0.000000000000000000, 0.001279392565614386563, 0.002558785131228773126, 0.003838177696843159473, 0.004477873979650353296, 0.005117570262457546253 ),
 .UNSPECIFIED. ) ;
#2743=ADVANCED_FACE ( 'NONE', ( #3164 ), #3259, .T. ) ;
#2745=AXIS2_PLACEMENT_3D ( 'NONE', #5842, #6661, #8769 ) ;
#2752=AXIS2_PLACEMENT_3D ( 'NONE', #2000, #7089, #9198 ) ;
#2765=DIRECTION ( 'NONE',  ( 1.000000000000000000, 0.000000000000000000, 0.000000000000000000 ) ) ;
#2773=CYLINDRICAL_SURFACE ( 'NONE', #4093, 2.999999999999999112 ) ;
#2776=DIRECTION ( 'NONE',  ( 0.000000000000000000, 0.000000000000000000, -1.000000000000000000 ) ) ;
#2778=FACE_OUTER_BOUND ( 'NONE', #5610, .T. ) ;
#2780=AXIS2_PLACEMENT_3D ( 'NONE', #2290, #1565, #1464 ) ;
#2786=CARTESIAN_POINT ( 'NONE',  ( -22.50000000000000000, -7.855833012397050680E-14, 5.000000000000000000 ) ) ;
#2795=DIRECTION ( 'NONE',  ( -0.000000000000000000, -0.000000000000000000, -1.000000000000000000 ) ) ;
#2808=DIRECTION ( 'NONE',  ( -1.000000000000000000, 0.000000000000000000, 0.000000000000000000 ) ) ;
#2809=CARTESIAN_POINT ( 'NONE',  ( 19.50000000000000355, 2.356749903719115078E-13, 5.000000000000000000 ) ) ;
#2811=CARTESIAN_POINT ( 'NONE',  ( -1.463718181065716051, -28.32253049495585273, 1.359567973934762142 ) ) ;
#2813=CIRCLE ( 'NONE', #2967, 6.000000000000000888 ) ;
#2817=CARTESIAN_POINT ( 'NONE',  ( 0.000000000000000000, 0.000000000000000000, 20.00000000000000000 ) ) ;
#2842=CARTESIAN_POINT ( 'NONE',  ( -19.50000000000000000, -7.819093608422630136E-14, 15.00000000000000000 ) ) ;
#2846=EDGE_CURVE ( 'NONE', #5930, #5682, #7774, .T. ) ;
#2851=VERTEX_POINT ( 'NONE', #468 ) ;
#2859=CARTESIAN_POINT ( 'NONE',  ( 1.072052546109581117, -28.40723195920986655, 1.426690145881926552 ) ) ;
#2861=ORIENTED_EDGE ( 'NONE', *, *, #2544, .T. ) ;
#2863=CARTESIAN_POINT ( 'NONE',  ( -27.81412668510618502, -2.815004828058397468, 0.9535900900804862301 ) ) ;
#2866=CIRCLE ( 'NONE', #7457, 6.000000000000001776 ) ;
#2869=DIRECTION ( 'NONE',  ( -0.000000000000000000, -0.000000000000000000, -1.000000000000000000 ) ) ;
#2871=ORIENTED_EDGE ( 'NONE', *, *, #2306, .F. ) ;
#2878=AXIS2_PLACEMENT_3D ( 'NONE', #4076, #3212, #6960 ) ;
#2883=ORIENTED_EDGE ( 'NONE', *, *, #5481, .T. ) ;
#2901=EDGE_CURVE ( 'NONE', #1107, #4182, #6820, .T. ) ;
#2918=DIRECTION ( 'NONE',  ( 0.000000000000000000, 0.000000000000000000, -1.000000000000000000 ) ) ;
#2929=DIRECTION ( 'NONE',  ( 0.000000000000000000, 0.000000000000000000, -1.000000000000000000 ) ) ;
#2949=DIRECTION ( 'NONE',  ( -1.000000000000000000, 0.000000000000000000, 0.000000000000000000 ) ) ;
#2961=CARTESIAN_POINT ( 'NONE',  ( 0.000000000000000000, 22.50000000000000355, 5.000000000000000000 ) ) ;
#2967=AXIS2_PLACEMENT_3D ( 'NONE', #2415, #252, #966 ) ;
#2975=AXIS2_PLACEMENT_3D ( 'NONE', #4464, #5810, #3739 ) ;
#3002=EDGE_CURVE ( 'NONE', #5323, #8143, #6061, .T. ) ;
#3026=AXIS2_PLACEMENT_3D ( 'NONE', #583, #7794, #4951 ) ;
#3044=EDGE_CURVE ( 'NONE', #5200, #754, #5288, .T. ) ;
#3048=CIRCLE ( 'NONE', #7675, 26.99999999999997868 ) ;
#3053=CARTESIAN_POINT ( 'NONE',  ( 2.060470863510026174, 28.13894063079881391, 1.213559982043999952 ) ) ;
#3054=EDGE_LOOP ( 'NONE', ( #4141, #4486, #1243, #4327 ) ) ;
#3056=DIRECTION ( 'NONE',  ( -1.000000000000000000, 0.000000000000000000, 0.000000000000000000 ) ) ;
#3079=AXIS2_PLACEMENT_3D ( 'NONE', #5119, #6573, #9394 ) ;
#3087=EDGE_LOOP ( 'NONE', ( #8205, #8824, #6605, #1657 ) ) ;
#3099=CARTESIAN_POINT ( 'NONE',  ( 22.50000000000000355, 2.356749903719115078E-13, 0.000000000000000000 ) ) ;
#3107=DIRECTION ( 'NONE',  ( -1.000000000000000000, 0.000000000000000000, 0.000000000000000000 ) ) ;
#3117=CARTESIAN_POINT ( 'NONE',  ( 0.000000000000000000, 0.000000000000000000, 10.00000000000000000 ) ) ;
#3121=AXIS2_PLACEMENT_3D ( 'NONE', #1899, #547, #4831 ) ;
#3125=CARTESIAN_POINT ( 'NONE',  ( 0.000000000000000000, 22.50000000000000355, 15.00000000000000000 ) ) ;
#3153=CYLINDRICAL_SURFACE ( 'NONE', #2745, 6.000000000000001776 ) ;
#3160=FACE_BOUND ( 'NONE', #3555, .T. ) ;
#3164=FACE_OUTER_BOUND ( 'NONE', #1257, .T. ) ;
#3173=CARTESIAN_POINT ( 'NONE',  ( 22.50000000000000355, 2.356749903719115078E-13, 10.00000000000000000 ) ) ;
#3175=DIRECTION ( 'NONE',  ( -0.000000000000000000, -0.000000000000000000, -1.000000000000000000 ) ) ;
#3180=EDGE_CURVE ( 'NONE', #2727, #4405, #9263, .T. ) ;
#3184=MANIFOLD_SOLID_BREP ( 'Radyus1', #5479 ) ;
#3201=CARTESIAN_POINT ( 'NONE',  ( 28.27439555746435929, 1.684082973785338444, 1.321420441384549838 ) ) ;
#3209=FACE_BOUND ( 'NONE', #3564, .T. ) ;
#3212=DIRECTION ( 'NONE',  ( 0.000000000000000000, 0.000000000000000000, -1.000000000000000000 ) ) ;
#3250=ORIENTED_EDGE ( 'NONE', *, *, #5595, .F. ) ;
#3252=ORIENTED_EDGE ( 'NONE', *, *, #4958, .T. ) ;
#3255=AXIS2_PLACEMENT_3D ( 'NONE', #4377, #3661, #8792 ) ;
#3259=CYLINDRICAL_SURFACE ( 'NONE', #4673, 30.00000000000000000 ) ;
#3272=FACE_BOUND ( 'NONE', #503, .T. ) ;
#3298=CIRCLE ( 'NONE', #4213, 2.999999999999999112 ) ;
#3301=EDGE_LOOP ( 'NONE', ( #5702, #5339, #4736, #8337 ) ) ;
#3320=LINE ( 'NONE', #4858, #8013 ) ;
#3322=CYLINDRICAL_SURFACE ( 'NONE', #6258, 15.00000000000000000 ) ;
#3339=AXIS2_PLACEMENT_3D ( 'NONE', #7681, #7728, #4031 ) ;
#3349=AXIS2_PLACEMENT_3D ( 'NONE', #7770, #7183, #1180 ) ;
#3351=CARTESIAN_POINT ( 'NONE',  ( 16.50000000000000000, 2.356749903719115078E-13, 0.000000000000000000 ) ) ;
#3357=EDGE_LOOP ( 'NONE', ( #2380, #7571 ) ) ;
#3368=ORIENTED_EDGE ( 'NONE', *, *, #2220, .F. ) ;
#3379=DIRECTION ( 'NONE',  ( 1.000000000000000000, 0.000000000000000000, 0.000000000000000000 ) ) ;
#3382=CARTESIAN_POINT ( 'NONE',  ( 1.571166602479410136E-13, -22.50000000000000355, 0.000000000000000000 ) ) ;
#3383=DIRECTION ( 'NONE',  ( -0.000000000000000000, -0.000000000000000000, -1.000000000000000000 ) ) ;
#3389=DIRECTION ( 'NONE',  ( -0.000000000000000000, -0.000000000000000000, -1.000000000000000000 ) ) ;
#3398=VECTOR ( 'NONE', #2617, 1000.000000000000000 ) ;
#3415=AXIS2_PLACEMENT_3D ( 'NONE', #7893, #8663, #2765 ) ;
#3422=EDGE_LOOP ( 'NONE', ( #1531, #6213, #3686, #671 ) ) ;
#3440=DIRECTION ( 'NONE',  ( -1.000000000000000000, 0.000000000000000000, 0.000000000000000000 ) ) ;
#3446=EDGE_CURVE ( 'NONE', #9313, #5080, #9464, .T. ) ;
#3457=CARTESIAN_POINT ( 'NONE',  ( -3.000000000000000000, 22.50000000000000355, 15.00000000000000000 ) ) ;
#3458=VECTOR ( 'NONE', #7206, 1000.000000000000000 ) ;
#3477=CARTESIAN_POINT ( 'NONE',  ( -3.000000000000000000, 22.50000000000000355, 10.00000000000000000 ) ) ;
#3482=CARTESIAN_POINT ( 'NONE',  ( 22.50000000000000355, 2.356749903719115078E-13, 5.000000000000000000 ) ) ;
#3483=DIRECTION ( 'NONE',  ( -0.7071067811865469066, 0.000000000000000000, -0.7071067811865481278 ) ) ;
#3486=VECTOR ( 'NONE', #2687, 1000.000000000000000 ) ;
#3492=CIRCLE ( 'NONE', #8262, 6.000000000000001776 ) ;
#3494=CARTESIAN_POINT ( 'NONE',  ( 3.000000000000156763, -22.50000000000000355, 15.00000000000000000 ) ) ;
#3502=EDGE_CURVE ( 'NONE', #6148, #5058, #1382, .T. ) ;
#3516=VERTEX_POINT ( 'NONE', #5856 ) ;
#3517=CARTESIAN_POINT ( 'NONE',  ( 1.571166602479410136E-13, -22.50000000000000355, 5.000000000000000000 ) ) ;
#3521=CARTESIAN_POINT ( 'NONE',  ( -16.49999999999999645, -7.782354204448209592E-14, 5.000000000000000000 ) ) ;
#3523=CARTESIAN_POINT ( 'NONE',  ( 4.333301281932962823, -26.64999999999994529, 0.000000000000000000 ) ) ;
#3536=EDGE_CURVE ( 'NONE', #9413, #1969, #6723, .T. ) ;
#3538=CARTESIAN_POINT ( 'NONE',  ( 0.000000000000000000, 22.50000000000000355, 5.000000000000000000 ) ) ;
#3540=CARTESIAN_POINT ( 'NONE',  ( 1.571166602479410136E-13, -22.50000000000000355, 5.000000000000000000 ) ) ;
#3542=EDGE_LOOP ( 'NONE', ( #4856, #8578 ) ) ;
#3555=EDGE_LOOP ( 'NONE', ( #6424, #762 ) ) ;
#3557=CARTESIAN_POINT ( 'NONE',  ( 28.06144414093874673, -2.260912237343545073, 1.151721138160509916 ) ) ;
#3564=EDGE_LOOP ( 'NONE', ( #901, #7141 ) ) ;
#3578=CARTESIAN_POINT ( 'NONE',  ( -26.91700667250954027, -4.077589154199041666, 0.2225055604246516383 ) ) ;
#3587=ORIENTED_EDGE ( 'NONE', *, *, #4505, .F. ) ;
#3594=VECTOR ( 'NONE', #6326, 1000.000000000000000 ) ;
#3605=CARTESIAN_POINT ( 'NONE',  ( -28.48867854402453403, -0.4256064988643077363, 1.491066224433648557 ) ) ;
#3621=CARTESIAN_POINT ( 'NONE',  ( 0.000000000000000000, 0.000000000000000000, 10.00000000000000000 ) ) ;
#3624=LINE ( 'NONE', #3767, #1169 ) ;
#3627=CARTESIAN_POINT ( 'NONE',  ( -28.44339478698104884, -0.8493939025103932616, 1.455282208020838741 ) ) ;
#3656=EDGE_CURVE ( 'NONE', #4735, #5058, #4263, .T. ) ;
#3660=DIRECTION ( 'NONE',  ( 0.000000000000000000, 0.000000000000000000, -1.000000000000000000 ) ) ;
#3661=DIRECTION ( 'NONE',  ( -0.000000000000000000, -0.000000000000000000, -1.000000000000000000 ) ) ;
#3671=VECTOR ( 'NONE', #6166, 1000.000000000000000 ) ;
#3683=CARTESIAN_POINT ( 'NONE',  ( 0.000000000000000000, 0.000000000000000000, 10.00000000000000000 ) ) ;
#3686=ORIENTED_EDGE ( 'NONE', *, *, #2846, .T. ) ;
#3705=CARTESIAN_POINT ( 'NONE',  ( 6.000000000000000888, 22.50000000000000355, 5.000000000000000000 ) ) ;
#3712=EDGE_CURVE ( 'NONE', #6154, #4625, #7478, .T. ) ;
#3721=CARTESIAN_POINT ( 'NONE',  ( 1.463718181065913226, 28.32253049495584918, 1.359567973934761698 ) ) ;
#3739=DIRECTION ( 'NONE',  ( -1.000000000000000000, 0.000000000000000000, 0.000000000000000000 ) ) ;
#3743=ORIENTED_EDGE ( 'NONE', *, *, #6871, .T. ) ;
#3745=ADVANCED_FACE ( 'NONE', ( #4888 ), #7792, .T. ) ;
#3760=CARTESIAN_POINT ( 'NONE',  ( -28.50000000000000000, -7.855833971761515132E-14, 1.500000000000037748 ) ) ;
#3766=ORIENTED_EDGE ( 'NONE', *, *, #2306, .T. ) ;
#3767=CARTESIAN_POINT ( 'NONE',  ( 6.000000000000157208, -22.50000000000000355, 5.000000000000000000 ) ) ;
#3782=( GEOMETRIC_REPRESENTATION_CONTEXT ( 3 ) GLOBAL_UNCERTAINTY_ASSIGNED_CONTEXT ( ( #5956 ) ) GLOBAL_UNIT_ASSIGNED_CONTEXT ( ( #1747, #1606, #4015 ) ) REPRESENTATION_CONTEXT ( 'NONE', 'WORKASPACE' ) );
#3794=CARTESIAN_POINT ( 'NONE',  ( 26.65000000000001634, -4.333301281932499194, 0.000000000000000000 ) ) ;
#3815=ORIENTED_EDGE ( 'NONE', *, *, #3180, .T. ) ;
#3816=ORIENTED_EDGE ( 'NONE', *, *, #8322, .F. ) ;
#3838=CARTESIAN_POINT ( 'NONE',  ( 15.00000000000000000, 1.836970198721029589E-15, 20.00000000000000000 ) ) ;
#3843=EDGE_CURVE ( 'NONE', #5058, #4735, #621, .T. ) ;
#3844=PRODUCT_CONTEXT ( 'NONE', #2480, 'mechanical' ) ;
#3852=CARTESIAN_POINT ( 'NONE',  ( -1.665361372754348812, -28.26799472218765175, 1.316292147329112483 ) ) ;
#3868=CARTESIAN_POINT ( 'NONE',  ( 22.50000000000000355, 2.356749903719115078E-13, 5.000000000000000000 ) ) ;
#3871=DIRECTION ( 'NONE',  ( -1.000000000000000000, 0.000000000000000000, 0.000000000000000000 ) ) ;
#3874=CIRCLE ( 'NONE', #5096, 26.99999999999997868 ) ;
#3878=DIRECTION ( 'NONE',  ( -1.000000000000000000, 0.000000000000000000, 0.000000000000000000 ) ) ;
#3881=ORIENTED_EDGE ( 'NONE', *, *, #3502, .F. ) ;
#3884=ADVANCED_FACE ( 'NONE', ( #2778 ), #6460, .T. ) ;
#3896=CARTESIAN_POINT ( 'NONE',  ( 0.000000000000000000, 0.000000000000000000, 10.00000000000000000 ) ) ;
#3901=DIRECTION ( 'NONE',  ( -1.000000000000000000, 0.000000000000000000, 0.000000000000000000 ) ) ;
#3902=ORIENTED_EDGE ( 'NONE', *, *, #1535, .T. ) ;
#3903=CARTESIAN_POINT ( 'NONE',  ( -3.000000000000000000, 22.50000000000000355, 5.000000000000000000 ) ) ;
#3918=DIRECTION ( 'NONE',  ( 0.000000000000000000, 0.000000000000000000, -1.000000000000000000 ) ) ;
#3920=CARTESIAN_POINT ( 'NONE',  ( 0.000000000000000000, 0.000000000000000000, 20.00000000000000000 ) ) ;
#3922=ADVANCED_FACE ( 'NONE', ( #6433 ), #5667, .T. ) ;
#3970=ADVANCED_FACE ( 'NONE', ( #1270 ), #698, .F. ) ;
#3973=FACE_OUTER_BOUND ( 'NONE', #3542, .T. ) ;
#3977=DIRECTION ( 'NONE',  ( -0.000000000000000000, -0.000000000000000000, -1.000000000000000000 ) ) ;
#4009=EDGE_CURVE ( 'NONE', #6154, #1500, #8297, .T. ) ;
#4015=( NAMED_UNIT ( * ) SI_UNIT ( $, .STERADIAN. ) SOLID_ANGLE_UNIT ( ) );
#4031=DIRECTION ( 'NONE',  ( 0.000000000000000000, 0.000000000000000000, -1.000000000000000000 ) ) ;
#4060=DIRECTION ( 'NONE',  ( 0.000000000000000000, 0.000000000000000000, 1.000000000000000000 ) ) ;
#4064=LINE ( 'NONE', #5606, #5900 ) ;
#4067=ORIENTED_EDGE ( 'NONE', *, *, #5113, .F. ) ;
#4075=DIRECTION ( 'NONE',  ( 0.000000000000000000, 0.000000000000000000, -1.000000000000000000 ) ) ;
#4076=CARTESIAN_POINT ( 'NONE',  ( 0.000000000000000000, 0.000000000000000000, 10.00000000000000000 ) ) ;
#4092=LINE ( 'NONE', #7070, #8320 ) ;
#4093=AXIS2_PLACEMENT_3D ( 'NONE', #4116, #7857, #6331 ) ;
#4101=ORIENTED_EDGE ( 'NONE', *, *, #3002, .T. ) ;
#4103=ORIENTED_EDGE ( 'NONE', *, *, #7618, .T. ) ;
#4104=AXIS2_PLACEMENT_3D ( 'NONE', #7247, #667, #5811 ) ;
#4111=LINE ( 'NONE', #456, #3594 ) ;
#4116=CARTESIAN_POINT ( 'NONE',  ( 22.50000000000000355, 2.356749903719115078E-13, 15.00000000000000000 ) ) ;
#4122=FACE_OUTER_BOUND ( 'NONE', #2240, .T. ) ;
#4128=EDGE_CURVE ( 'NONE', #5535, #4476, #4615, .T. ) ;
#4141=ORIENTED_EDGE ( 'NONE', *, *, #9442, .F. ) ;
#4162=EDGE_LOOP ( 'NONE', ( #7799, #9153, #1844, #3902 ) ) ;
#4167=DIRECTION ( 'NONE',  ( 1.000000000000000000, 0.000000000000000000, -0.000000000000000000 ) ) ;
#4177=LINE ( 'NONE', #1284, #8088 ) ;
#4178=ORIENTED_EDGE ( 'NONE', *, *, #6729, .F. ) ;
#4182=VERTEX_POINT ( 'NONE', #1708 ) ;
#4186=TOROIDAL_SURFACE ( 'NONE', #6495, 16.00000000000000000, 1.000000000000000000 ) ;
#4197=DIRECTION ( 'NONE',  ( -0.000000000000000000, -0.000000000000000000, -1.000000000000000000 ) ) ;
#4212=ORIENTED_EDGE ( 'NONE', *, *, #7704, .F. ) ;
#4213=AXIS2_PLACEMENT_3D ( 'NONE', #3173, #7496, #9076 ) ;
#4229=CARTESIAN_POINT ( 'NONE',  ( 6.000000000000157208, -22.50000000000000355, 0.000000000000000000 ) ) ;
#4238=EDGE_CURVE ( 'NONE', #883, #5050, #5849, .T. ) ;
#4258=CONICAL_SURFACE ( 'NONE', #3026, 28.00000000000000711, 0.7853981633974473908 ) ;
#4259=FACE_OUTER_BOUND ( 'NONE', #5873, .T. ) ;
#4263=CIRCLE ( 'NONE', #6116, 2.999999999999999556 ) ;
#4264=DIRECTION ( 'NONE',  ( -1.000000000000000000, 0.000000000000000000, 0.000000000000000000 ) ) ;
#4272=CIRCLE ( 'NONE', #5652, 6.000000000000001776 ) ;
#4275=VECTOR ( 'NONE', #2229, 1000.000000000000114 ) ;
#4285=CARTESIAN_POINT ( 'NONE',  ( 28.13653351783517209, -2.066994717595015629, 1.211640400093609848 ) ) ;
#4295=CIRCLE ( 'NONE', #8728, 30.00000000000000000 ) ;
#4307=CARTESIAN_POINT ( 'NONE',  ( -26.64999999999995950, -4.333301281932866900, 0.000000000000000000 ) ) ;
#4308=AXIS2_PLACEMENT_3D ( 'NONE', #4977, #5846, #4167 ) ;
#4327=ORIENTED_EDGE ( 'NONE', *, *, #7153, .T. ) ;
#4332=DIRECTION ( 'NONE',  ( -1.000000000000000000, 0.000000000000000000, 0.000000000000000000 ) ) ;
#4335=EDGE_CURVE ( 'NONE', #4745, #5080, #7806, .T. ) ;
#4337=ORIENTED_EDGE ( 'NONE', *, *, #2121, .T. ) ;
#4345=CARTESIAN_POINT ( 'NONE',  ( 1.691658612279592466, -28.27209108258186276, 1.319590333518659397 ) ) ;
#4349=CARTESIAN_POINT ( 'NONE',  ( 0.8460976106428692578, 28.45495154861555420, 1.464499174736009879 ) ) ;
#4351=CARTESIAN_POINT ( 'NONE',  ( -27.61161645726460989, -3.165483362335529183, 0.7903941804162353257 ) ) ;
#4355=AXIS2_PLACEMENT_3D ( 'NONE', #7854, #2721, #5561 ) ;
#4373=ORIENTED_EDGE ( 'NONE', *, *, #5942, .F. ) ;
#4377=CARTESIAN_POINT ( 'NONE',  ( -22.50000000000000000, -7.855833012397050680E-14, 5.000000000000000000 ) ) ;
#4386=CARTESIAN_POINT ( 'NONE',  ( -4.333301281932778082, 26.64999999999997371, 0.000000000000000000 ) ) ;
#4392=CARTESIAN_POINT ( 'NONE',  ( 1.571166602479410136E-13, -22.50000000000000355, 5.000000000000000000 ) ) ;
#4401=DIRECTION ( 'NONE',  ( 1.000000000000000000, 0.000000000000000000, 0.000000000000000000 ) ) ;
#4403=CIRCLE ( 'NONE', #1486, 2.999999999999999556 ) ;
#4405=VERTEX_POINT ( 'NONE', #595 ) ;
#4410=AXIS2_PLACEMENT_3D ( 'NONE', #2786, #5720, #8634 ) ;
#4413=ADVANCED_FACE ( 'NONE', ( #1260 ), #5787, .F. ) ;
#4430=LINE ( 'NONE', #2366, #6024 ) ;
#4447=CARTESIAN_POINT ( 'NONE',  ( 2.813989238837719675, 27.81487630015519841, 0.9541967664096193680 ) ) ;
#4464=CARTESIAN_POINT ( 'NONE',  ( -22.50000000000000000, -7.855833012397050680E-14, 15.00000000000000000 ) ) ;
#4476=VERTEX_POINT ( 'NONE', #4386 ) ;
#4486=ORIENTED_EDGE ( 'NONE', *, *, #6999, .F. ) ;
#4496=DIRECTION ( 'NONE',  ( 0.000000000000000000, 0.000000000000000000, -1.000000000000000000 ) ) ;
#4505=EDGE_CURVE ( 'NONE', #8041, #2851, #27, .T. ) ;
#4526=DIRECTION ( 'NONE',  ( 0.000000000000000000, 0.000000000000000000, -1.000000000000000000 ) ) ;
#4527=DIRECTION ( 'NONE',  ( -1.000000000000000000, 0.000000000000000000, -0.000000000000000000 ) ) ;
#4539=DIRECTION ( 'NONE',  ( 1.000000000000000000, 0.000000000000000000, 0.000000000000000000 ) ) ;
#4552=ORIENTED_EDGE ( 'NONE', *, *, #7107, .F. ) ;
#4557=CARTESIAN_POINT ( 'NONE',  ( -30.00000000000000000, 0.000000000000000000, 3.000000000000052847 ) ) ;
#4576=CARTESIAN_POINT ( 'NONE',  ( 4.078200081724819626, -26.91636876093598119, 0.2219739674467010593 ) ) ;
#4615=CIRCLE ( 'NONE', #773, 6.000000000000000888 ) ;
#4617=APPLICATION_CONTEXT ( 'automotive_design' ) ;
#4625=VERTEX_POINT ( 'NONE', #5449 ) ;
#4628=DIRECTION ( 'NONE',  ( -0.000000000000000000, -0.000000000000000000, -1.000000000000000000 ) ) ;
#4629=DIRECTION ( 'NONE',  ( -0.000000000000000000, -0.000000000000000000, -1.000000000000000000 ) ) ;
#4634=AXIS2_PLACEMENT_3D ( 'NONE', #1349, #9269, #5689 ) ;
#4642=DIRECTION ( 'NONE',  ( 1.000000000000000000, 0.000000000000000000, 0.000000000000000000 ) ) ;
#4662=ORIENTED_EDGE ( 'NONE', *, *, #2469, .F. ) ;
#4673=AXIS2_PLACEMENT_3D ( 'NONE', #3117, #5523, #6055 ) ;
#4676=EDGE_CURVE ( 'NONE', #6525, #6171, #3048, .T. ) ;
#4691=CARTESIAN_POINT ( 'NONE',  ( 28.50000000000000355, 2.364097880450372804E-13, 1.500000000000041078 ) ) ;
#4735=VERTEX_POINT ( 'NONE', #8701 ) ;
#4736=ORIENTED_EDGE ( 'NONE', *, *, #3843, .T. ) ;
#4745=VERTEX_POINT ( 'NONE', #1983 ) ;
#4775=CARTESIAN_POINT ( 'NONE',  ( -15.00000000000000000, 0.000000000000000000, 20.00000000000000000 ) ) ;
#4790=VERTEX_POINT ( 'NONE', #6316 ) ;
#4799=VERTEX_POINT ( 'NONE', #4229 ) ;
#4800=CIRCLE ( 'NONE', #656, 1.000000000000000888 ) ;
#4811=CIRCLE ( 'NONE', #6051, 2.999999999999999112 ) ;
#4818=EDGE_LOOP ( 'NONE', ( #625, #3815 ) ) ;
#4828=FACE_OUTER_BOUND ( 'NONE', #8862, .T. ) ;
#4831=DIRECTION ( 'NONE',  ( 1.000000000000000000, 0.000000000000000000, 0.000000000000000000 ) ) ;
#4833=VERTEX_POINT ( 'NONE', #631 ) ;
#4835=ORIENTED_EDGE ( 'NONE', *, *, #7543, .T. ) ;
#4839=PLANE ( 'NONE',  #2554 ) ;
#4840=DIRECTION ( 'NONE',  ( -1.000000000000000000, 0.000000000000000000, 0.000000000000000000 ) ) ;
#4852=AXIS2_PLACEMENT_3D ( 'NONE', #1582, #155, #7491 ) ;
#4856=ORIENTED_EDGE ( 'NONE', *, *, #6550, .T. ) ;
#4858=CARTESIAN_POINT ( 'NONE',  ( -2.999999999999842792, -22.50000000000000355, 15.00000000000000000 ) ) ;
#4873=AXIS2_PLACEMENT_3D ( 'NONE', #7873, #620, #8781 ) ;
#4880=FACE_OUTER_BOUND ( 'NONE', #3422, .T. ) ;
#4888=FACE_OUTER_BOUND ( 'NONE', #5223, .T. ) ;
#4925=CARTESIAN_POINT ( 'NONE',  ( -2.819222834329253136, 27.81181297095831084, 0.9517275379012117842 ) ) ;
#4926=ORIENTED_EDGE ( 'NONE', *, *, #1240, .T. ) ;
#4934=ORIENTED_EDGE ( 'NONE', *, *, #3446, .F. ) ;
#4935=AXIS2_PLACEMENT_3D ( 'NONE', #6696, #5982, #781 ) ;
#4940=EDGE_CURVE ( 'NONE', #1266, #5535, #7494, .T. ) ;
#4942=DIRECTION ( 'NONE',  ( -0.000000000000000000, -0.000000000000000000, -1.000000000000000000 ) ) ;
#4951=DIRECTION ( 'NONE',  ( -1.000000000000000000, 0.000000000000000000, 0.000000000000000000 ) ) ;
#4958=EDGE_CURVE ( 'NONE', #6408, #3516, #4295, .T. ) ;
#4970=CARTESIAN_POINT ( 'NONE',  ( -0.8594978869055871495, 28.44192451354557605, 1.454119780865612999 ) ) ;
#4977=CARTESIAN_POINT ( 'NONE',  ( 0.000000000000000000, 0.000000000000000000, 20.00000000000000000 ) ) ;
#4989=DIRECTION ( 'NONE',  ( -0.000000000000000000, -0.000000000000000000, -1.000000000000000000 ) ) ;
#4991=ORIENTED_EDGE ( 'NONE', *, *, #9233, .T. ) ;
#4997=CARTESIAN_POINT ( 'NONE',  ( 28.50000000000000711, -0.4241759143233731488, 1.500000000000038192 ) ) ;
#5012=DIRECTION ( 'NONE',  ( 0.000000000000000000, 0.000000000000000000, 1.000000000000000000 ) ) ;
#5026=AXIS2_PLACEMENT_3D ( 'NONE', #5081, #7334, #5278 ) ;
#5034=AXIS2_PLACEMENT_3D ( 'NONE', #6096, #6955, #3878 ) ;
#5041=DIRECTION ( 'NONE',  ( -1.000000000000000000, 0.000000000000000000, 0.000000000000000000 ) ) ;
#5050=VERTEX_POINT ( 'NONE', #5437 ) ;
#5051=AXIS2_PLACEMENT_3D ( 'NONE', #3896, #3175, #7692 ) ;
#5053=LINE ( 'NONE', #2116, #3458 ) ;
#5058=VERTEX_POINT ( 'NONE', #1776 ) ;
#5065=EDGE_CURVE ( 'NONE', #4799, #6171, #8356, .T. ) ;
#5071=CARTESIAN_POINT ( 'NONE',  ( 16.50000000000000000, 2.356749903719115078E-13, 5.000000000000000000 ) ) ;
#5080=VERTEX_POINT ( 'NONE', #8270 ) ;
#5081=CARTESIAN_POINT ( 'NONE',  ( 0.000000000000000000, 22.50000000000000355, 5.000000000000000000 ) ) ;
#5086=ORIENTED_EDGE ( 'NONE', *, *, #5315, .F. ) ;
#5096=AXIS2_PLACEMENT_3D ( 'NONE', #8650, #2795, #6981 ) ;
#5113=EDGE_CURVE ( 'NONE', #5930, #5629, #3298, .T. ) ;
#5119=CARTESIAN_POINT ( 'NONE',  ( 0.000000000000000000, 0.000000000000000000, 3.000000000000052847 ) ) ;
#5122=FACE_OUTER_BOUND ( 'NONE', #3054, .T. ) ;
#5131=STYLED_ITEM('',(#9522),#3184);
#5141=LINE ( 'NONE', #2842, #94 ) ;
#5161=CARTESIAN_POINT ( 'NONE',  ( 1.665361372754546654, 28.26799472218765530, 1.316292147329111373 ) ) ;
#5167=AXIS2_PLACEMENT_3D ( 'NONE', #641, #6415, #3379 ) ;
#5170=CIRCLE ( 'NONE', #114, 15.00000000000000000 ) ;
#5174=EDGE_LOOP ( 'NONE', ( #6242, #4103, #6139, #7067, #4178 ) ) ;
#5187=ORIENTED_EDGE ( 'NONE', *, *, #2347, .F. ) ;
#5200=VERTEX_POINT ( 'NONE', #2651 ) ;
#5201=VECTOR ( 'NONE', #926, 1000.000000000000000 ) ;
#5205=DIRECTION ( 'NONE',  ( 1.000000000000000000, 0.000000000000000000, 0.000000000000000000 ) ) ;
#5208=ORIENTED_EDGE ( 'NONE', *, *, #6651, .T. ) ;
#5223=EDGE_LOOP ( 'NONE', ( #2219, #5887, #1868, #5525 ) ) ;
#5249=CARTESIAN_POINT ( 'NONE',  ( 3.168636005459071203, -27.60958896060100543, 0.7887504010224316575 ) ) ;
#5266=AXIS2_PLACEMENT_3D ( 'NONE', #820, #4526, #1401 ) ;
#5269=DIRECTION ( 'NONE',  ( 0.000000000000000000, 0.000000000000000000, 1.000000000000000000 ) ) ;
#5273=AXIS2_PLACEMENT_3D ( 'NONE', #3621, #6470, #208 ) ;
#5278=DIRECTION ( 'NONE',  ( -1.000000000000000000, 0.000000000000000000, 0.000000000000000000 ) ) ;
#5281=DIRECTION ( 'NONE',  ( -1.000000000000000000, 0.000000000000000000, 0.000000000000000000 ) ) ;
#5288=CIRCLE ( 'NONE', #1445, 2.999999999999999112 ) ;
#5293=DIRECTION ( 'NONE',  ( 1.000000000000000000, 0.000000000000000000, 0.000000000000000000 ) ) ;
#5297=CARTESIAN_POINT ( 'NONE',  ( -0.8460976106426699728, -28.45495154861555065, 1.464499174736009879 ) ) ;
#5304=DIRECTION ( 'NONE',  ( 1.000000000000000000, 0.000000000000000000, 0.000000000000000000 ) ) ;
#5315=EDGE_CURVE ( 'NONE', #5682, #1677, #6824, .T. ) ;
#5319=CARTESIAN_POINT ( 'NONE',  ( 22.50000000000000355, 2.356749903719115078E-13, 5.000000000000000000 ) ) ;
#5322=CARTESIAN_POINT ( 'NONE',  ( -22.50000000000000000, -7.855833012397050680E-14, 15.00000000000000000 ) ) ;
#5323=VERTEX_POINT ( 'NONE', #9007 ) ;
#5332=DIRECTION ( 'NONE',  ( 0.000000000000000000, 0.000000000000000000, -1.000000000000000000 ) ) ;
#5338=ORIENTED_EDGE ( 'NONE', *, *, #4009, .F. ) ;
#5339=ORIENTED_EDGE ( 'NONE', *, *, #3502, .T. ) ;
#5364=ORIENTED_EDGE ( 'NONE', *, *, #3536, .T. ) ;
#5365=SHAPE_REPRESENTATION_RELATIONSHIP ( 'NONE' , 'NONE' ,  #6964, #7497 ) ;
#5372=FACE_BOUND ( 'NONE', #740, .T. ) ;
#5381=CARTESIAN_POINT ( 'NONE',  ( 0.000000000000000000, 0.000000000000000000, 10.00000000000000000 ) ) ;
#5388=ORIENTED_EDGE ( 'NONE', *, *, #144, .F. ) ;
#5406=ORIENTED_EDGE ( 'NONE', *, *, #6729, .T. ) ;
#5408=CARTESIAN_POINT ( 'NONE',  ( -28.50000000000000000, -7.855833971761515132E-14, 1.500000000000037748 ) ) ;
#5412=CARTESIAN_POINT ( 'NONE',  ( 0.000000000000000000, 0.000000000000000000, 11.00000000000000000 ) ) ;
#5414=CARTESIAN_POINT ( 'NONE',  ( 3.000000000000000000, 22.50000000000000355, 10.00000000000000000 ) ) ;
#5418=CARTESIAN_POINT ( 'NONE',  ( -22.50000000000000000, -7.855833012397050680E-14, 0.000000000000000000 ) ) ;
#5422=DIRECTION ( 'NONE',  ( -1.000000000000000000, 0.000000000000000000, 0.000000000000000000 ) ) ;
#5437=CARTESIAN_POINT ( 'NONE',  ( -19.50000000000000000, -7.819093608422630136E-14, 10.00000000000000000 ) ) ;
#5449=CARTESIAN_POINT ( 'NONE',  ( 16.00000000000000000, 0.000000000000000000, 9.999999999999998224 ) ) ;
#5462=CARTESIAN_POINT ( 'NONE',  ( 0.000000000000000000, 0.000000000000000000, 8.000000000000005329 ) ) ;
#5479=CLOSED_SHELL ( 'NONE', ( #7061, #8698, #8274, #3970, #2605, #2023, #6072, #8134, #6776, #6830, #4413, #714, #1237, #2743, #596, #2369, #8642, #3922, #2140, #8234, #1902, #7730, #6224, #364, #1839, #8457, #9348, #2563, #2028, #9068, #3884, #3745, #5528 ) ) ;
#5481=EDGE_CURVE ( 'NONE', #5629, #1677, #4064, .T. ) ;
#5492=PLANE ( 'NONE',  #4410 ) ;
#5504=DIRECTION ( 'NONE',  ( 0.000000000000000000, 0.000000000000000000, 1.000000000000000000 ) ) ;
#5523=DIRECTION ( 'NONE',  ( -0.000000000000000000, -0.000000000000000000, -1.000000000000000000 ) ) ;
#5525=ORIENTED_EDGE ( 'NONE', *, *, #7044, .F. ) ;
#5528=ADVANCED_FACE ( 'NONE', ( #4828 ), #7746, .F. ) ;
#5535=VERTEX_POINT ( 'NONE', #7613 ) ;
#5543=EDGE_CURVE ( 'NONE', #2498, #720, #2736, .T. ) ;
#5547=VECTOR ( 'NONE', #9279, 1000.000000000000000 ) ;
#5553=EDGE_CURVE ( 'NONE', #106, #2851, #8803, .T. ) ;
#5559=CARTESIAN_POINT ( 'NONE',  ( 27.61161645726459568, 3.165483362335713480, 0.7903941804162394336 ) ) ;
#5561=DIRECTION ( 'NONE',  ( -1.000000000000000000, 0.000000000000000000, 0.000000000000000000 ) ) ;
#5595=EDGE_CURVE ( 'NONE', #7535, #7179, #4111, .T. ) ;
#5601=FACE_OUTER_BOUND ( 'NONE', #5752, .T. ) ;
#5606=CARTESIAN_POINT ( 'NONE',  ( 25.50000000000000355, 2.360423844116556880E-13, 15.00000000000000000 ) ) ;
#5610=EDGE_LOOP ( 'NONE', ( #2871, #5919, #3368, #8444, #491, #8871, #8720, #6380 ) ) ;
#5622=ORIENTED_EDGE ( 'NONE', *, *, #3712, .T. ) ;
#5629=VERTEX_POINT ( 'NONE', #7951 ) ;
#5633=EDGE_LOOP ( 'NONE', ( #6322, #4926, #2009, #524 ) ) ;
#5652=AXIS2_PLACEMENT_3D ( 'NONE', #3482, #2776, #7861 ) ;
#5659=CARTESIAN_POINT ( 'NONE',  ( -3.795548148769716690, 27.16282829747752103, 0.4246316111951826122 ) ) ;
#5667=PLANE ( 'NONE',  #4308 ) ;
#5682=VERTEX_POINT ( 'NONE', #2809 ) ;
#5689=DIRECTION ( 'NONE',  ( -1.000000000000000000, 0.000000000000000000, 0.000000000000000000 ) ) ;
#5695=CARTESIAN_POINT ( 'NONE',  ( 0.000000000000000000, 0.000000000000000000, 11.00000000000000000 ) ) ;
#5696=CARTESIAN_POINT ( 'NONE',  ( -27.81257783158192254, 2.818165554823761632, 0.9523463990989800010 ) ) ;
#5702=ORIENTED_EDGE ( 'NONE', *, *, #8390, .T. ) ;
#5703=ORIENTED_EDGE ( 'NONE', *, *, #9233, .F. ) ;
#5704=CARTESIAN_POINT ( 'NONE',  ( -1.691658612279394402, 28.27209108258186987, 1.319590333518658065 ) ) ;
#5711=EDGE_CURVE ( 'NONE', #9400, #4833, #7383, .T. ) ;
#5713=CARTESIAN_POINT ( 'NONE',  ( 6.000000000000000888, 22.50000000000000355, 5.000000000000000000 ) ) ;
#5716=ORIENTED_EDGE ( 'NONE', *, *, #5595, .T. ) ;
#5720=DIRECTION ( 'NONE',  ( 0.000000000000000000, 0.000000000000000000, -1.000000000000000000 ) ) ;
#5726=EDGE_LOOP ( 'NONE', ( #5897, #9047, #166, #7763 ) ) ;
#5748=CARTESIAN_POINT ( 'NONE',  ( 0.8594978869057854354, -28.44192451354556539, 1.454119780865607447 ) ) ;
#5752=EDGE_LOOP ( 'NONE', ( #3816, #3766, #4212, #7359, #648, #2385, #6920, #817 ) ) ;
#5754=DIRECTION ( 'NONE',  ( -1.000000000000000000, 0.000000000000000000, 0.000000000000000000 ) ) ;
#5767=CARTESIAN_POINT ( 'NONE',  ( 3.000000000000000000, 22.50000000000000355, 15.00000000000000000 ) ) ;
#5774=EDGE_CURVE ( 'NONE', #1969, #9413, #6173, .T. ) ;
#5787=CYLINDRICAL_SURFACE ( 'NONE', #8758, 6.000000000000001776 ) ;
#5791=CARTESIAN_POINT ( 'NONE',  ( -2.813989238837524276, -27.81487630015522328, 0.9541967664096193680 ) ) ;
#5802=DIRECTION ( 'NONE',  ( 0.000000000000000000, 0.000000000000000000, 1.000000000000000000 ) ) ;
#5810=DIRECTION ( 'NONE',  ( -0.000000000000000000, -0.000000000000000000, -1.000000000000000000 ) ) ;
#5811=DIRECTION ( 'NONE',  ( 1.000000000000000000, 0.000000000000000000, 0.000000000000000000 ) ) ;
#5822=B_SPLINE_CURVE_WITH_KNOTS ( 'NONE', 3,
 ( #9437, #3578, #6516, #4351, #2863, #8724, #2141, #695, #3627, #3605, #7609, #5408 ),
 .UNSPECIFIED., .F., .F.,
 ( 4, 2, 2, 2, 2, 4 ),
 ( 9.098896311893213187E-19, 0.001279392565614375721, 0.002558785131228750575, 0.003838177696843125212, 0.004477873979650310796, 0.005117570262457497680 ),
 .UNSPECIFIED. ) ;
#5842=CARTESIAN_POINT ( 'NONE',  ( -22.50000000000000000, -7.855833012397050680E-14, 5.000000000000000000 ) ) ;
#5846=DIRECTION ( 'NONE',  ( 0.000000000000000000, 0.000000000000000000, 1.000000000000000000 ) ) ;
#5849=CIRCLE ( 'NONE', #7073, 2.999999999999999112 ) ;
#5850=DIRECTION ( 'NONE',  ( -1.000000000000000000, 0.000000000000000000, 0.000000000000000000 ) ) ;
#5856=CARTESIAN_POINT ( 'NONE',  ( 30.00000000000000000, 3.673940397442059178E-15, 3.000000000000052847 ) ) ;
#5857=CYLINDRICAL_SURFACE ( 'NONE', #2975, 2.999999999999999112 ) ;
#5869=CYLINDRICAL_SURFACE ( 'NONE', #3255, 6.000000000000001776 ) ;
#5873=EDGE_LOOP ( 'NONE', ( #7085, #1659, #6910, #4373 ) ) ;
#5874=CARTESIAN_POINT ( 'NONE',  ( -4.333301281932591564, -26.65000000000000213, 0.000000000000000000 ) ) ;
#5887=ORIENTED_EDGE ( 'NONE', *, *, #3002, .F. ) ;
#5897=ORIENTED_EDGE ( 'NONE', *, *, #1535, .F. ) ;
#5900=VECTOR ( 'NONE', #3977, 1000.000000000000000 ) ;
#5903=AXIS2_PLACEMENT_3D ( 'NONE', #3683, #5802, #4401 ) ;
#5919=ORIENTED_EDGE ( 'NONE', *, *, #907, .F. ) ;
#5930=VERTEX_POINT ( 'NONE', #7557 ) ;
#5942=EDGE_CURVE ( 'NONE', #4405, #1500, #8323, .T. ) ;
#5951=AXIS2_PLACEMENT_3D ( 'NONE', #3540, #8154, #8008 ) ;
#5956=UNCERTAINTY_MEASURE_WITH_UNIT (LENGTH_MEASURE( 1.000000000000000082E-05 ), #1747, 'distance_accuracy_value', 'NONE');
#5963=CARTESIAN_POINT ( 'NONE',  ( 28.50000000000000355, 2.364097880450372804E-13, 1.500000000000041078 ) ) ;
#5982=DIRECTION ( 'NONE',  ( 0.000000000000000000, 0.000000000000000000, 1.000000000000000000 ) ) ;
#6020=CARTESIAN_POINT ( 'NONE',  ( 0.2247925377430787797, -28.49955466461978304, 1.499648419317237913 ) ) ;
#6024=VECTOR ( 'NONE', #2165, 1000.000000000000114 ) ;
#6031=ORIENTED_EDGE ( 'NONE', *, *, #4335, .F. ) ;
#6051=AXIS2_PLACEMENT_3D ( 'NONE', #227, #6093, #2445 ) ;
#6055=DIRECTION ( 'NONE',  ( -1.000000000000000000, 0.000000000000000000, 0.000000000000000000 ) ) ;
#6061=CIRCLE ( 'NONE', #5903, 28.00000000000000711 ) ;
#6072=ADVANCED_FACE ( 'NONE', ( #585 ), #1299, .F. ) ;
#6082=VERTEX_POINT ( 'NONE', #632 ) ;
#6090=CIRCLE ( 'NONE', #8377, 6.000000000000001776 ) ;
#6092=DIRECTION ( 'NONE',  ( 0.000000000000000000, 0.000000000000000000, 1.000000000000000000 ) ) ;
#6093=DIRECTION ( 'NONE',  ( 0.000000000000000000, 0.000000000000000000, 1.000000000000000000 ) ) ;
#6096=CARTESIAN_POINT ( 'NONE',  ( 22.50000000000000355, 2.356749903719115078E-13, 0.000000000000000000 ) ) ;
#6099=FACE_BOUND ( 'NONE', #6400, .T. ) ;
#6116=AXIS2_PLACEMENT_3D ( 'NONE', #2401, #5332, #5281 ) ;
#6139=ORIENTED_EDGE ( 'NONE', *, *, #7669, .T. ) ;
#6148=VERTEX_POINT ( 'NONE', #8131 ) ;
#6154=VERTEX_POINT ( 'NONE', #13 ) ;
#6166=DIRECTION ( 'NONE',  ( -0.000000000000000000, -0.000000000000000000, -1.000000000000000000 ) ) ;
#6171=VERTEX_POINT ( 'NONE', #1492 ) ;
#6173=CIRCLE ( 'NONE', #4935, 3.000000000000000000 ) ;
#6190=FACE_OUTER_BOUND ( 'NONE', #2309, .T. ) ;
#6194=ORIENTED_EDGE ( 'NONE', *, *, #5553, .F. ) ;
#6195=EDGE_CURVE ( 'NONE', #8143, #4833, #4430, .T. ) ;
#6199=CIRCLE ( 'NONE', #3121, 26.99999999999997868 ) ;
#6209=CARTESIAN_POINT ( 'NONE',  ( 0.000000000000000000, 0.000000000000000000, 0.000000000000000000 ) ) ;
#6212=FACE_OUTER_BOUND ( 'NONE', #717, .T. ) ;
#6213=ORIENTED_EDGE ( 'NONE', *, *, #2469, .T. ) ;
#6224=ADVANCED_FACE ( 'NONE', ( #1640 ), #5869, .F. ) ;
#6228=DIRECTION ( 'NONE',  ( 0.000000000000000000, 0.000000000000000000, -1.000000000000000000 ) ) ;
#6229=DIRECTION ( 'NONE',  ( -0.000000000000000000, -0.000000000000000000, -1.000000000000000000 ) ) ;
#6242=ORIENTED_EDGE ( 'NONE', *, *, #6522, .F. ) ;
#6249=CIRCLE ( 'NONE', #2091, 2.999999999999999556 ) ;
#6258=AXIS2_PLACEMENT_3D ( 'NONE', #6274, #1296, #7071 ) ;
#6264=FACE_OUTER_BOUND ( 'NONE', #1989, .T. ) ;
#6274=CARTESIAN_POINT ( 'NONE',  ( 0.000000000000000000, 0.000000000000000000, 20.00000000000000000 ) ) ;
#6280=EDGE_LOOP ( 'NONE', ( #4101, #9325 ) ) ;
#6283=DIRECTION ( 'NONE',  ( -1.000000000000000000, 0.000000000000000000, 0.000000000000000000 ) ) ;
#6293=CARTESIAN_POINT ( 'NONE',  ( -19.50000000000000000, -7.819093608422630136E-14, 5.000000000000000000 ) ) ;
#6316=CARTESIAN_POINT ( 'NONE',  ( -2.999999999999842792, -22.50000000000000355, 10.00000000000000000 ) ) ;
#6322=ORIENTED_EDGE ( 'NONE', *, *, #5711, .T. ) ;
#6323=CARTESIAN_POINT ( 'NONE',  ( -16.00000000000000000, 1.959434878635765131E-15, 11.00000000000000000 ) ) ;
#6326=DIRECTION ( 'NONE',  ( -0.000000000000000000, -0.000000000000000000, -1.000000000000000000 ) ) ;
#6331=DIRECTION ( 'NONE',  ( -1.000000000000000000, 0.000000000000000000, 0.000000000000000000 ) ) ;
#6336=DIRECTION ( 'NONE',  ( 0.000000000000000000, 0.000000000000000000, -1.000000000000000000 ) ) ;
#6352=ORIENTED_EDGE ( 'NONE', *, *, #7741, .F. ) ;
#6353=CARTESIAN_POINT ( 'NONE',  ( -28.50000000000000000, -7.855833012397050680E-14, 5.000000000000000000 ) ) ;
#6379=CARTESIAN_POINT ( 'NONE',  ( -4.078200081724630444, 26.91636876093601316, 0.2219739674467013368 ) ) ;
#6380=ORIENTED_EDGE ( 'NONE', *, *, #4958, .F. ) ;
#6395=FACE_OUTER_BOUND ( 'NONE', #8821, .T. ) ;
#6400=EDGE_LOOP ( 'NONE', ( #1408, #471 ) ) ;
#6408=VERTEX_POINT ( 'NONE', #4557 ) ;
#6415=DIRECTION ( 'NONE',  ( -0.000000000000000000, -0.000000000000000000, 1.000000000000000000 ) ) ;
#6424=ORIENTED_EDGE ( 'NONE', *, *, #3536, .F. ) ;
#6433=FACE_OUTER_BOUND ( 'NONE', #4818, .T. ) ;
#6454=DIRECTION ( 'NONE',  ( -0.000000000000000000, -0.000000000000000000, -1.000000000000000000 ) ) ;
#6460=CONICAL_SURFACE ( 'NONE', #3079, 30.00000000000000000, 0.7853981633974428389 ) ;
#6470=DIRECTION ( 'NONE',  ( -0.000000000000000000, -0.000000000000000000, -1.000000000000000000 ) ) ;
#6492=DIRECTION ( 'NONE',  ( 0.000000000000000000, 0.000000000000000000, 1.000000000000000000 ) ) ;
#6495=AXIS2_PLACEMENT_3D ( 'NONE', #5695, #5012, #8570 ) ;
#6498=CARTESIAN_POINT ( 'NONE',  ( 27.81257783158193675, -2.818165554823583552, 0.9523463990989768924 ) ) ;
#6501=VECTOR ( 'NONE', #2320, 1000.000000000000114 ) ;
#6508=CARTESIAN_POINT ( 'NONE',  ( -28.06144414093873962, 2.260912237343719600, 1.151721138160513469 ) ) ;
#6516=CARTESIAN_POINT ( 'NONE',  ( -27.16400976452049321, -3.794195651236124789, 0.4256031388450376984 ) ) ;
#6522=EDGE_CURVE ( 'NONE', #1857, #777, #3492, .T. ) ;
#6525=VERTEX_POINT ( 'NONE', #1135 ) ;
#6544=DIRECTION ( 'NONE',  ( -0.000000000000000000, -0.000000000000000000, 1.000000000000000000 ) ) ;
#6550=EDGE_CURVE ( 'NONE', #777, #1857, #4272, .T. ) ;
#6553=CIRCLE ( 'NONE', #8212, 6.000000000000000000 ) ;
#6562=CARTESIAN_POINT ( 'NONE',  ( -4.077745023575802819, -26.91684391854058589, 0.2223699321171553334 ) ) ;
#6568=AXIS2_PLACEMENT_3D ( 'NONE', #3125, #2410, #8932 ) ;
#6571=CARTESIAN_POINT ( 'NONE',  ( -5.999999999999842792, -22.50000000000000355, 5.000000000000000000 ) ) ;
#6573=DIRECTION ( 'NONE',  ( -0.000000000000000000, -0.000000000000000000, 1.000000000000000000 ) ) ;
#6587=VERTEX_POINT ( 'NONE', #4307 ) ;
#6603=EDGE_LOOP ( 'NONE', ( #1387, #7953 ) ) ;
#6605=ORIENTED_EDGE ( 'NONE', *, *, #5711, .F. ) ;
#6607=DIRECTION ( 'NONE',  ( 0.000000000000000000, 0.000000000000000000, 1.000000000000000000 ) ) ;
#6612=CARTESIAN_POINT ( 'NONE',  ( 3.157268078127849265, 27.61694991999677029, 0.7947205175373169839 ) ) ;
#6651=EDGE_CURVE ( 'NONE', #4745, #7535, #1499, .T. ) ;
#6657=ORIENTED_EDGE ( 'NONE', *, *, #4335, .T. ) ;
#6661=DIRECTION ( 'NONE',  ( -0.000000000000000000, -0.000000000000000000, -1.000000000000000000 ) ) ;
#6670=ORIENTED_EDGE ( 'NONE', *, *, #7626, .T. ) ;
#6689=ORIENTED_EDGE ( 'NONE', *, *, #2846, .F. ) ;
#6696=CARTESIAN_POINT ( 'NONE',  ( 0.000000000000000000, 22.50000000000000355, 10.00000000000000000 ) ) ;
#6705=DIRECTION ( 'NONE',  ( -1.000000000000000000, 0.000000000000000000, 0.000000000000000000 ) ) ;
#6709=EDGE_CURVE ( 'NONE', #720, #3516, #7465, .T. ) ;
#6723=CIRCLE ( 'NONE', #4873, 3.000000000000000000 ) ;
#6724=EDGE_CURVE ( 'NONE', #6525, #7742, #1504, .T. ) ;
#6729=EDGE_CURVE ( 'NONE', #777, #7742, #8002, .T. ) ;
#6732=PRODUCT_DEFINITION_CONTEXT ( 'detailed design', #4617, 'design' ) ;
#6739=AXIS2_PLACEMENT_3D ( 'NONE', #2339, #5269, #8192 ) ;
#6760=CARTESIAN_POINT ( 'NONE',  ( 0.000000000000000000, 0.000000000000000000, 0.000000000000000000 ) ) ;
#6769=CARTESIAN_POINT ( 'NONE',  ( 1.571166602479410136E-13, -22.50000000000000355, 15.00000000000000000 ) ) ;
#6776=ADVANCED_FACE ( 'NONE', ( #1462 ), #3153, .F. ) ;
#6788=CARTESIAN_POINT ( 'NONE',  ( -3.791949971500568228, -27.16611547376998814, 0.4273392542514636294 ) ) ;
#6791=ORIENTED_EDGE ( 'NONE', *, *, #6724, .F. ) ;
#6820=CIRCLE ( 'NONE', #9255, 6.000000000000000888 ) ;
#6824=CIRCLE ( 'NONE', #8969, 2.999999999999999112 ) ;
#6830=ADVANCED_FACE ( 'NONE', ( #8864 ), #2285, .F. ) ;
#6833=EDGE_CURVE ( 'NONE', #8143, #5323, #1351, .T. ) ;
#6855=PLANE ( 'NONE',  #1784 ) ;
#6863=CIRCLE ( 'NONE', #1022, 6.000000000000000888 ) ;
#6871=EDGE_CURVE ( 'NONE', #1677, #5682, #1817, .T. ) ;
#6885=CARTESIAN_POINT ( 'NONE',  ( 6.000000000000000888, 22.50000000000000355, 0.000000000000000000 ) ) ;
#6907=CARTESIAN_POINT ( 'NONE',  ( 28.48867854402453759, 0.4256064988644707725, 1.491066224433653442 ) ) ;
#6910=ORIENTED_EDGE ( 'NONE', *, *, #4009, .T. ) ;
#6911=CARTESIAN_POINT ( 'NONE',  ( -26.64999999999998792, 4.333301281932682159, 0.000000000000000000 ) ) ;
#6920=ORIENTED_EDGE ( 'NONE', *, *, #9419, .F. ) ;
#6940=ORIENTED_EDGE ( 'NONE', *, *, #3044, .F. ) ;
#6941=EDGE_LOOP ( 'NONE', ( #8010, #7540, #146, #1793 ) ) ;
#6944=CARTESIAN_POINT ( 'NONE',  ( 1.571166602479410136E-13, -22.50000000000000355, 10.00000000000000000 ) ) ;
#6955=DIRECTION ( 'NONE',  ( 0.000000000000000000, 0.000000000000000000, -1.000000000000000000 ) ) ;
#6960=DIRECTION ( 'NONE',  ( -1.000000000000000000, 0.000000000000000000, 0.000000000000000000 ) ) ;
#6962=AXIS2_PLACEMENT_3D ( 'NONE', #9306, #4942, #7875 ) ;
#6964=SHAPE_REPRESENTATION ( '5-Cover', ( #1614 ), #3782 ) ;
#6979=LINE ( 'NONE', #565, #1186 ) ;
#6980=ORIENTED_EDGE ( 'NONE', *, *, #9221, .F. ) ;
#6981=DIRECTION ( 'NONE',  ( 1.000000000000000000, 0.000000000000000000, 0.000000000000000000 ) ) ;
#6998=ORIENTED_EDGE ( 'NONE', *, *, #9221, .T. ) ;
#6999=EDGE_CURVE ( 'NONE', #8041, #1701, #206, .T. ) ;
#7004=CARTESIAN_POINT ( 'NONE',  ( 1.571166602479410136E-13, -22.50000000000000355, 5.000000000000000000 ) ) ;
#7043=DIRECTION ( 'NONE',  ( -1.000000000000000000, 0.000000000000000000, 0.000000000000000000 ) ) ;
#7044=EDGE_CURVE ( 'NONE', #4833, #9400, #2189, .T. ) ;
#7053=ORIENTED_EDGE ( 'NONE', *, *, #9457, .F. ) ;
#7059=ORIENTED_EDGE ( 'NONE', *, *, #4676, .T. ) ;
#7061=ADVANCED_FACE ( 'NONE', ( #592 ), #4186, .F. ) ;
#7067=ORIENTED_EDGE ( 'NONE', *, *, #6724, .T. ) ;
#7070=CARTESIAN_POINT ( 'NONE',  ( -30.00000000000000000, 0.000000000000000000, 10.00000000000000000 ) ) ;
#7071=DIRECTION ( 'NONE',  ( -1.000000000000000000, 0.000000000000000000, 0.000000000000000000 ) ) ;
#7073=AXIS2_PLACEMENT_3D ( 'NONE', #2487, #7612, #4642 ) ;
#7074=( LENGTH_UNIT ( ) NAMED_UNIT ( * ) SI_UNIT ( .MILLI., .METRE. ) );
#7085=ORIENTED_EDGE ( 'NONE', *, *, #3180, .F. ) ;
#7089=DIRECTION ( 'NONE',  ( -0.000000000000000000, -0.000000000000000000, -1.000000000000000000 ) ) ;
#7093=CIRCLE ( 'NONE', #5266, 6.000000000000000000 ) ;
#7107=EDGE_CURVE ( 'NONE', #1500, #2573, #4800, .T. ) ;
#7116=ORIENTED_EDGE ( 'NONE', *, *, #9442, .T. ) ;
#7120=ORIENTED_EDGE ( 'NONE', *, *, #5553, .T. ) ;
#7141=ORIENTED_EDGE ( 'NONE', *, *, #2262, .T. ) ;
#7153=EDGE_CURVE ( 'NONE', #2851, #4799, #7093, .T. ) ;
#7179=VERTEX_POINT ( 'NONE', #3760 ) ;
#7183=DIRECTION ( 'NONE',  ( 0.000000000000000000, 0.000000000000000000, -1.000000000000000000 ) ) ;
#7184=AXIS2_PLACEMENT_3D ( 'NONE', #2485, #6228, #2576 ) ;
#7196=B_SPLINE_CURVE_WITH_KNOTS ( 'NONE', 3,
 ( #1991, #7947, #2713, #2080, #8613, #1259, #6508, #5696, #7804, #9234, #7850, #1306 ),
 .UNSPECIFIED., .F., .F.,
 ( 4, 2, 2, 2, 2, 4 ),
 ( 0.005117570262457497680, 0.006390849577664777653, 0.007027489235268418941, 0.007664128892872060228, 0.008937408208079342803, 0.01021068752328662538 ),
 .UNSPECIFIED. ) ;
#7206=DIRECTION ( 'NONE',  ( -0.000000000000000000, -0.000000000000000000, -1.000000000000000000 ) ) ;
#7247=CARTESIAN_POINT ( 'NONE',  ( 0.000000000000000000, 0.000000000000000000, 11.00000000000000000 ) ) ;
#7252=ORIENTED_EDGE ( 'NONE', *, *, #4238, .T. ) ;
#7253=DIRECTION ( 'NONE',  ( -1.000000000000000000, 0.000000000000000000, 0.000000000000000000 ) ) ;
#7271=CARTESIAN_POINT ( 'NONE',  ( 2.254970896015934478, 28.06387613437634343, 1.153664892585073654 ) ) ;
#7292=ORIENTED_EDGE ( 'NONE', *, *, #7545, .T. ) ;
#7300=VECTOR ( 'NONE', #3483, 1000.000000000000114 ) ;
#7304=DIRECTION ( 'NONE',  ( 0.000000000000000000, 0.000000000000000000, -1.000000000000000000 ) ) ;
#7306=EDGE_LOOP ( 'NONE', ( #6031, #2021, #5716, #8167, #7511 ) ) ;
#7310=ORIENTED_EDGE ( 'NONE', *, *, #6651, .F. ) ;
#7332=ORIENTED_EDGE ( 'NONE', *, *, #4128, .T. ) ;
#7334=DIRECTION ( 'NONE',  ( 0.000000000000000000, 0.000000000000000000, -1.000000000000000000 ) ) ;
#7357=CARTESIAN_POINT ( 'NONE',  ( 0.000000000000000000, 22.50000000000000355, 0.000000000000000000 ) ) ;
#7359=ORIENTED_EDGE ( 'NONE', *, *, #6709, .F. ) ;
#7367=VERTEX_POINT ( 'NONE', #3903 ) ;
#7368=DIRECTION ( 'NONE',  ( -0.000000000000000000, -0.000000000000000000, -1.000000000000000000 ) ) ;
#7377=CARTESIAN_POINT ( 'NONE',  ( 28.50000000000000355, 2.364097784513999692E-13, 5.000000000000000000 ) ) ;
#7383=CIRCLE ( 'NONE', #8920, 30.00000000000000000 ) ;
#7388=UNCERTAINTY_MEASURE_WITH_UNIT (LENGTH_MEASURE( 1.000000000000000082E-05 ), #7074, 'distance_accuracy_value', 'NONE');
#7407=DIRECTION ( 'NONE',  ( 0.000000000000000000, 0.000000000000000000, -1.000000000000000000 ) ) ;
#7413=ORIENTED_EDGE ( 'NONE', *, *, #6999, .T. ) ;
#7424=CYLINDRICAL_SURFACE ( 'NONE', #9098, 2.999999999999999112 ) ;
#7444=EDGE_CURVE ( 'NONE', #9400, #6408, #4092, .T. ) ;
#7449=ORIENTED_EDGE ( 'NONE', *, *, #907, .T. ) ;
#7450=ORIENTED_EDGE ( 'NONE', *, *, #6550, .F. ) ;
#7451=CIRCLE ( 'NONE', #1777, 30.00000000000000000 ) ;
#7457=AXIS2_PLACEMENT_3D ( 'NONE', #5418, #1084, #366 ) ;
#7465=LINE ( 'NONE', #890, #4275 ) ;
#7478=CIRCLE ( 'NONE', #3339, 1.000000000000000888 ) ;
#7491=DIRECTION ( 'NONE',  ( -1.000000000000000000, 0.000000000000000000, 0.000000000000000000 ) ) ;
#7494=CIRCLE ( 'NONE', #442, 6.000000000000000888 ) ;
#7496=DIRECTION ( 'NONE',  ( 0.000000000000000000, 0.000000000000000000, 1.000000000000000000 ) ) ;
#7497=ADVANCED_BREP_SHAPE_REPRESENTATION ( '', ( #3184, #1614 ), #3782 ) ;
#7511=ORIENTED_EDGE ( 'NONE', *, *, #3446, .T. ) ;
#7523=DIRECTION ( 'NONE',  ( -1.000000000000000000, 0.000000000000000000, 0.000000000000000000 ) ) ;
#7532=CARTESIAN_POINT ( 'NONE',  ( 22.50000000000000355, 2.356749903719115078E-13, 5.000000000000000000 ) ) ;
#7535=VERTEX_POINT ( 'NONE', #6353 ) ;
#7540=ORIENTED_EDGE ( 'NONE', *, *, #1824, .T. ) ;
#7543=EDGE_CURVE ( 'NONE', #4790, #4735, #3320, .T. ) ;
#7545=EDGE_CURVE ( 'NONE', #9313, #4476, #3874, .T. ) ;
#7549=DIRECTION ( 'NONE',  ( 0.000000000000000000, 0.000000000000000000, 1.000000000000000000 ) ) ;
#7557=CARTESIAN_POINT ( 'NONE',  ( 19.50000000000000355, 2.356749903719115078E-13, 10.00000000000000000 ) ) ;
#7571=ORIENTED_EDGE ( 'NONE', *, *, #3843, .F. ) ;
#7580=EDGE_CURVE ( 'NONE', #5050, #754, #5141, .T. ) ;
#7593=FACE_OUTER_BOUND ( 'NONE', #5633, .T. ) ;
#7595=PLANE ( 'NONE',  #2671 ) ;
#7609=CARTESIAN_POINT ( 'NONE',  ( -28.50000000000001066, -0.2131062308234238922, 1.500000000000038858 ) ) ;
#7612=DIRECTION ( 'NONE',  ( 0.000000000000000000, 0.000000000000000000, 1.000000000000000000 ) ) ;
#7613=CARTESIAN_POINT ( 'NONE',  ( -6.000000000000000888, 22.50000000000000355, 0.000000000000000000 ) ) ;
#7617=ORIENTED_EDGE ( 'NONE', *, *, #5113, .T. ) ;
#7618=EDGE_CURVE ( 'NONE', #1857, #720, #5053, .T. ) ;
#7626=EDGE_CURVE ( 'NONE', #7535, #4745, #6090, .T. ) ;
#7650=AXIS2_PLACEMENT_3D ( 'NONE', #3099, #8725, #6705 ) ;
#7655=CARTESIAN_POINT ( 'NONE',  ( 0.000000000000000000, 0.000000000000000000, 10.00000000000000000 ) ) ;
#7669=EDGE_CURVE ( 'NONE', #720, #6525, #7693, .T. ) ;
#7671=DIRECTION ( 'NONE',  ( 0.000000000000000000, 0.000000000000000000, 1.000000000000000000 ) ) ;
#7675=AXIS2_PLACEMENT_3D ( 'NONE', #392, #4629, #8428 ) ;
#7678=FACE_BOUND ( 'NONE', #6603, .T. ) ;
#7681=CARTESIAN_POINT ( 'NONE',  ( 16.00000000000000000, 0.000000000000000000, 11.00000000000000000 ) ) ;
#7692=DIRECTION ( 'NONE',  ( -1.000000000000000000, 0.000000000000000000, 0.000000000000000000 ) ) ;
#7693=B_SPLINE_CURVE_WITH_KNOTS ( 'NONE', 3,
 ( #5963, #4997, #2162, #7928, #1346, #4285, #3557, #6498, #8023, #1439, #9027, #3794 ),
 .UNSPECIFIED., .F., .F.,
 ( 4, 2, 2, 2, 2, 4 ),
 ( 0.005117570262457546253, 0.006390849577664815817, 0.007027489235268451033, 0.007664128892872086249, 0.008937408208079361885, 0.01021068752328663752 ),
 .UNSPECIFIED. ) ;
#7704=EDGE_CURVE ( 'NONE', #3516, #6408, #7451, .T. ) ;
#7728=DIRECTION ( 'NONE',  ( 0.000000000000000000, -1.000000000000000000, 0.000000000000000000 ) ) ;
#7729=AXIS2_PLACEMENT_3D ( 'NONE', #2693, #2062, #8688 ) ;
#7730=ADVANCED_FACE ( 'NONE', ( #201, #4122 ), #4839, .T. ) ;
#7741=EDGE_CURVE ( 'NONE', #6082, #7367, #8076, .T. ) ;
#7742=VERTEX_POINT ( 'NONE', #3351 ) ;
#7746=TOROIDAL_SURFACE ( 'NONE', #828, 16.00000000000000000, 1.000000000000000000 ) ;
#7755=ORIENTED_EDGE ( 'NONE', *, *, #2053, .T. ) ;
#7763=ORIENTED_EDGE ( 'NONE', *, *, #3712, .F. ) ;
#7770=CARTESIAN_POINT ( 'NONE',  ( -22.50000000000000000, -7.855833012397050680E-14, 5.000000000000000000 ) ) ;
#7772=DIRECTION ( 'NONE',  ( 1.000000000000000000, 0.000000000000000000, 0.000000000000000000 ) ) ;
#7774=LINE ( 'NONE', #8542, #518 ) ;
#7784=CARTESIAN_POINT ( 'NONE',  ( 26.64999999999992752, 4.333301281933056970, 0.000000000000000000 ) ) ;
#7792=CONICAL_SURFACE ( 'NONE', #2878, 28.00000000000000711, 0.7853981633974473908 ) ;
#7794=DIRECTION ( 'NONE',  ( 0.000000000000000000, 0.000000000000000000, -1.000000000000000000 ) ) ;
#7799=ORIENTED_EDGE ( 'NONE', *, *, #1359, .F. ) ;
#7804=CARTESIAN_POINT ( 'NONE',  ( -27.61492299646193871, 3.160432959937508723, 0.7930775300198876776 ) ) ;
#7806=LINE ( 'NONE', #3521, #5547 ) ;
#7809=LINE ( 'NONE', #406, #8646 ) ;
#7827=EDGE_CURVE ( 'NONE', #5323, #9400, #2050, .T. ) ;
#7836=EDGE_LOOP ( 'NONE', ( #2460, #2204, #8692, #7848 ) ) ;
#7848=ORIENTED_EDGE ( 'NONE', *, *, #426, .T. ) ;
#7850=CARTESIAN_POINT ( 'NONE',  ( -26.91620486903880050, 4.078357040894757368, 0.2218373908656702531 ) ) ;
#7854=CARTESIAN_POINT ( 'NONE',  ( 22.50000000000000355, 2.356749903719115078E-13, 5.000000000000000000 ) ) ;
#7856=EDGE_LOOP ( 'NONE', ( #8031, #2620 ) ) ;
#7857=DIRECTION ( 'NONE',  ( -0.000000000000000000, -0.000000000000000000, -1.000000000000000000 ) ) ;
#7858=ORIENTED_EDGE ( 'NONE', *, *, #4940, .F. ) ;
#7861=DIRECTION ( 'NONE',  ( -1.000000000000000000, 0.000000000000000000, 0.000000000000000000 ) ) ;
#7873=CARTESIAN_POINT ( 'NONE',  ( 0.000000000000000000, 22.50000000000000355, 10.00000000000000000 ) ) ;
#7875=DIRECTION ( 'NONE',  ( -1.000000000000000000, 0.000000000000000000, 0.000000000000000000 ) ) ;
#7893=CARTESIAN_POINT ( 'NONE',  ( 0.000000000000000000, 0.000000000000000000, 8.000000000000005329 ) ) ;
#7901=CARTESIAN_POINT ( 'NONE',  ( -0.4367635713301901701, 28.48785780768279707, 1.490418226835894755 ) ) ;
#7910=LINE ( 'NONE', #5713, #3486 ) ;
#7918=CARTESIAN_POINT ( 'NONE',  ( -22.50000000000000000, -7.855833012397050680E-14, 0.000000000000000000 ) ) ;
#7923=EDGE_LOOP ( 'NONE', ( #5364, #2861, #164, #8073 ) ) ;
#7928=CARTESIAN_POINT ( 'NONE',  ( 28.32042821893189455, -1.471975546721147721, 1.357900206176151370 ) ) ;
#7947=CARTESIAN_POINT ( 'NONE',  ( -28.50000000000000000, 0.4241759143235341312, 1.500000000000036859 ) ) ;
#7951=CARTESIAN_POINT ( 'NONE',  ( 25.50000000000000355, 2.360423844116556880E-13, 10.00000000000000000 ) ) ;
#7952=CARTESIAN_POINT ( 'NONE',  ( -3.157268078127657862, -27.61694991999679871, 0.7947205175373147634 ) ) ;
#7953=ORIENTED_EDGE ( 'NONE', *, *, #8210, .F. ) ;
#7996=CARTESIAN_POINT ( 'NONE',  ( 3.795548148769905428, -27.16282829747748195, 0.4246316111951826677 ) ) ;
#8002=LINE ( 'NONE', #1414, #139 ) ;
#8008=DIRECTION ( 'NONE',  ( -1.000000000000000000, 0.000000000000000000, 0.000000000000000000 ) ) ;
#8010=ORIENTED_EDGE ( 'NONE', *, *, #2901, .F. ) ;
#8013=VECTOR ( 'NONE', #9369, 1000.000000000000000 ) ;
#8023=CARTESIAN_POINT ( 'NONE',  ( 27.61492299646195647, -3.160432959937327535, 0.7930775300198846800 ) ) ;
#8031=ORIENTED_EDGE ( 'NONE', *, *, #2347, .T. ) ;
#8039=AXIS2_PLACEMENT_3D ( 'NONE', #3382, #1170, #7043 ) ;
#8040=EDGE_LOOP ( 'NONE', ( #7310, #6657, #4991, #7449, #3250 ) ) ;
#8041=VERTEX_POINT ( 'NONE', #6571 ) ;
#8051=PRODUCT_DEFINITION ( 'UNKNOWN', '', #1002, #6732 ) ;
#8073=ORIENTED_EDGE ( 'NONE', *, *, #8651, .F. ) ;
#8076=CIRCLE ( 'NONE', #4852, 3.000000000000000000 ) ;
#8088=VECTOR ( 'NONE', #4989, 1000.000000000000000 ) ;
#8090=CARTESIAN_POINT ( 'NONE',  ( -5.999999999999842792, -22.50000000000000355, 5.000000000000000000 ) ) ;
#8091=CIRCLE ( 'NONE', #9303, 16.00000000000000000 ) ;
#8097=CARTESIAN_POINT ( 'NONE',  ( 4.077745023575991112, 26.91684391854055036, 0.2223699321171545285 ) ) ;
#8107=DIRECTION ( 'NONE',  ( -1.000000000000000000, 0.000000000000000000, 0.000000000000000000 ) ) ;
#8111=AXIS2_PLACEMENT_3D ( 'NONE', #8149, #1563, #3056 ) ;
#8131=CARTESIAN_POINT ( 'NONE',  ( 3.000000000000156763, -22.50000000000000355, 10.00000000000000000 ) ) ;
#8134=ADVANCED_FACE ( 'NONE', ( #8482 ), #1851, .F. ) ;
#8139=PLANE ( 'NONE',  #1177 ) ;
#8143=VERTEX_POINT ( 'NONE', #223 ) ;
#8144=ORIENTED_EDGE ( 'NONE', *, *, #3656, .T. ) ;
#8149=CARTESIAN_POINT ( 'NONE',  ( 1.571166602479410136E-13, -22.50000000000000355, 5.000000000000000000 ) ) ;
#8154=DIRECTION ( 'NONE',  ( -0.000000000000000000, -0.000000000000000000, -1.000000000000000000 ) ) ;
#8164=FACE_OUTER_BOUND ( 'NONE', #2357, .T. ) ;
#8165=CARTESIAN_POINT ( 'NONE',  ( -15.00000000000000000, 0.000000000000000000, 11.00000000000000000 ) ) ;
#8167=ORIENTED_EDGE ( 'NONE', *, *, #8322, .T. ) ;
#8176=CARTESIAN_POINT ( 'NONE',  ( -2.254970896015736415, -28.06387613437635409, 1.153664892585073432 ) ) ;
#8178=ORIENTED_EDGE ( 'NONE', *, *, #1123, .T. ) ;
#8180=B_SPLINE_CURVE_WITH_KNOTS ( 'NONE', 3,
 ( #504, #6379, #5659, #8580, #4925, #9341, #5704, #8622, #4970, #7901, #8903, #8860, #4349, #3721, #5161, #3053, #7271, #4447, #6612, #32, #8097, #693 ),
 .UNSPECIFIED., .F., .F.,
 ( 4, 2, 2, 2, 2, 2, 2, 2, 2, 2, 4 ),
 ( 0.000000000000000000, 0.001276335940410827955, 0.002552671880821655911, 0.003829007821232484950, 0.004467175791437899036, 0.005105343761643314424, 0.006381679702054142596, 0.007019847672259558850, 0.007658015642464973370, 0.008934351582875805012, 0.01021068752328663752 ),
 .UNSPECIFIED. ) ;
#8190=ORIENTED_EDGE ( 'NONE', *, *, #9419, .T. ) ;
#8192=DIRECTION ( 'NONE',  ( 1.000000000000000000, 0.000000000000000000, 0.000000000000000000 ) ) ;
#8203=CARTESIAN_POINT ( 'NONE',  ( 4.333301281932778082, 26.64999999999997371, 0.000000000000000000 ) ) ;
#8205=ORIENTED_EDGE ( 'NONE', *, *, #6833, .F. ) ;
#8210=EDGE_CURVE ( 'NONE', #6148, #4790, #6249, .T. ) ;
#8212=AXIS2_PLACEMENT_3D ( 'NONE', #4392, #4075, #2949 ) ;
#8233=EDGE_LOOP ( 'NONE', ( #1480, #5187, #4337, #7332, #8190, #1506 ) ) ;
#8234=ADVANCED_FACE ( 'NONE', ( #5372, #3973 ), #6855, .T. ) ;
#8250=DIRECTION ( 'NONE',  ( -0.000000000000000000, -0.000000000000000000, -1.000000000000000000 ) ) ;
#8262=AXIS2_PLACEMENT_3D ( 'NONE', #7532, #2497, #5422 ) ;
#8270=CARTESIAN_POINT ( 'NONE',  ( -16.49999999999999645, -7.782354204448209592E-14, 0.000000000000000000 ) ) ;
#8272=CYLINDRICAL_SURFACE ( 'NONE', #5051, 30.00000000000000000 ) ;
#8274=ADVANCED_FACE ( 'NONE', ( #5601 ), #558, .T. ) ;
#8288=DIRECTION ( 'NONE',  ( 0.000000000000000000, 0.000000000000000000, -1.000000000000000000 ) ) ;
#8297=CIRCLE ( 'NONE', #2780, 15.00000000000000000 ) ;
#8306=CARTESIAN_POINT ( 'NONE',  ( 25.50000000000000355, 2.360423844116556880E-13, 5.000000000000000000 ) ) ;
#8320=VECTOR ( 'NONE', #6454, 1000.000000000000000 ) ;
#8322=EDGE_CURVE ( 'NONE', #7179, #9313, #7196, .T. ) ;
#8323=LINE ( 'NONE', #4775, #3398 ) ;
#8334=CARTESIAN_POINT ( 'NONE',  ( 28.14436749771988033, 2.074924133079033339, 1.218150816307271178 ) ) ;
#8336=DIRECTION ( 'NONE',  ( -0.000000000000000000, -0.000000000000000000, -1.000000000000000000 ) ) ;
#8337=ORIENTED_EDGE ( 'NONE', *, *, #7543, .F. ) ;
#8341=DIRECTION ( 'NONE',  ( 0.000000000000000000, 0.000000000000000000, 1.000000000000000000 ) ) ;
#8356=CIRCLE ( 'NONE', #8666, 6.000000000000000000 ) ;
#8377=AXIS2_PLACEMENT_3D ( 'NONE', #10, #2929, #7253 ) ;
#8390=EDGE_CURVE ( 'NONE', #4790, #6148, #4403, .T. ) ;
#8428=DIRECTION ( 'NONE',  ( 1.000000000000000000, 0.000000000000000000, 0.000000000000000000 ) ) ;
#8441=CARTESIAN_POINT ( 'NONE',  ( 28.50000000000001066, 0.2131062308235842917, 1.500000000000043299 ) ) ;
#8444=ORIENTED_EDGE ( 'NONE', *, *, #2300, .F. ) ;
#8457=ADVANCED_FACE ( 'NONE', ( #2173, #1599 ), #8139, .T. ) ;
#8482=FACE_OUTER_BOUND ( 'NONE', #6941, .T. ) ;
#8484=CARTESIAN_POINT ( 'NONE',  ( 26.64999999999992752, 4.333301281933056970, 0.000000000000000000 ) ) ;
#8495=CARTESIAN_POINT ( 'NONE',  ( 1.571166602479410136E-13, -22.50000000000000355, 5.000000000000000000 ) ) ;
#8505=DIRECTION ( 'NONE',  ( 1.000000000000000000, 0.000000000000000000, 0.000000000000000000 ) ) ;
#8507=ORIENTED_EDGE ( 'NONE', *, *, #5065, .F. ) ;
#8516=( NAMED_UNIT ( * ) PLANE_ANGLE_UNIT ( ) SI_UNIT ( $, .RADIAN. ) );
#8522=DIRECTION ( 'NONE',  ( -1.000000000000000000, 1.224646799147353454E-16, 0.000000000000000000 ) ) ;
#8527=DIRECTION ( 'NONE',  ( 1.000000000000000000, 0.000000000000000000, 0.000000000000000000 ) ) ;
#8542=CARTESIAN_POINT ( 'NONE',  ( 19.50000000000000355, 2.356749903719115078E-13, 15.00000000000000000 ) ) ;
#8570=DIRECTION ( 'NONE',  ( 1.000000000000000000, 0.000000000000000000, 0.000000000000000000 ) ) ;
#8576=DIRECTION ( 'NONE',  ( 1.000000000000000000, 0.000000000000000000, 0.000000000000000000 ) ) ;
#8578=ORIENTED_EDGE ( 'NONE', *, *, #6522, .T. ) ;
#8579=ORIENTED_EDGE ( 'NONE', *, *, #310, .T. ) ;
#8580=CARTESIAN_POINT ( 'NONE',  ( -3.168636005458878024, 27.60958896060101964, 0.7887504010224319906 ) ) ;
#8585=DIRECTION ( 'NONE',  ( -0.000000000000000000, -0.000000000000000000, -1.000000000000000000 ) ) ;
#8588=EDGE_CURVE ( 'NONE', #4625, #2573, #8091, .T. ) ;
#8590=EDGE_LOOP ( 'NONE', ( #8902, #7450, #5406, #6998, #515 ) ) ;
#8594=CYLINDRICAL_SURFACE ( 'NONE', #6962, 2.999999999999999556 ) ;
#8613=CARTESIAN_POINT ( 'NONE',  ( -28.26575725008335027, 1.673027373762006054, 1.314514334795903183 ) ) ;
#8622=CARTESIAN_POINT ( 'NONE',  ( -1.072052546109382609, 28.40723195920987720, 1.426690145881925220 ) ) ;
#8634=DIRECTION ( 'NONE',  ( -1.000000000000000000, 0.000000000000000000, -0.000000000000000000 ) ) ;
#8641=CARTESIAN_POINT ( 'NONE',  ( -16.00000000000000000, 1.959434878635765131E-15, 9.999999999999998224 ) ) ;
#8642=ADVANCED_FACE ( 'NONE', ( #9130 ), #3322, .T. ) ;
#8646=VECTOR ( 'NONE', #3383, 1000.000000000000000 ) ;
#8650=CARTESIAN_POINT ( 'NONE',  ( 0.000000000000000000, 0.000000000000000000, 0.000000000000000000 ) ) ;
#8651=EDGE_CURVE ( 'NONE', #9413, #7367, #1248, .T. ) ;
#8663=DIRECTION ( 'NONE',  ( 0.000000000000000000, 0.000000000000000000, -1.000000000000000000 ) ) ;
#8666=AXIS2_PLACEMENT_3D ( 'NONE', #9121, #247, #339 ) ;
#8667=DIRECTION ( 'NONE',  ( 0.000000000000000000, 0.000000000000000000, -1.000000000000000000 ) ) ;
#8674=CARTESIAN_POINT ( 'NONE',  ( 28.50000000000000355, 2.364097880450372804E-13, 1.500000000000041078 ) ) ;
#8688=DIRECTION ( 'NONE',  ( 1.000000000000000000, 0.000000000000000000, 0.000000000000000000 ) ) ;
#8692=ORIENTED_EDGE ( 'NONE', *, *, #8651, .T. ) ;
#8698=ADVANCED_FACE ( 'NONE', ( #1205 ), #4258, .T. ) ;
#8701=CARTESIAN_POINT ( 'NONE',  ( -2.999999999999842792, -22.50000000000000355, 5.000000000000000000 ) ) ;
#8720=ORIENTED_EDGE ( 'NONE', *, *, #6709, .T. ) ;
#8724=CARTESIAN_POINT ( 'NONE',  ( -28.14436749771988389, -2.074924133078855704, 1.218150816307263851 ) ) ;
#8725=DIRECTION ( 'NONE',  ( 0.000000000000000000, 0.000000000000000000, -1.000000000000000000 ) ) ;
#8728=AXIS2_PLACEMENT_3D ( 'NONE', #8936, #6544, #5293 ) ;
#8756=CARTESIAN_POINT ( 'NONE',  ( 1.571166602479410136E-13, -22.50000000000000355, 10.00000000000000000 ) ) ;
#8758=AXIS2_PLACEMENT_3D ( 'NONE', #2133, #4197, #2808 ) ;
#8762=CARTESIAN_POINT ( 'NONE',  ( -30.00000000000000000, 3.673940397442059178E-15, 3.000000000000052847 ) ) ;
#8769=DIRECTION ( 'NONE',  ( -1.000000000000000000, 0.000000000000000000, 0.000000000000000000 ) ) ;
#8781=DIRECTION ( 'NONE',  ( 1.000000000000000000, 0.000000000000000000, 0.000000000000000000 ) ) ;
#8792=DIRECTION ( 'NONE',  ( -1.000000000000000000, 0.000000000000000000, 0.000000000000000000 ) ) ;
#8803=CIRCLE ( 'NONE', #8039, 6.000000000000000000 ) ;
#8820=CYLINDRICAL_SURFACE ( 'NONE', #1339, 6.000000000000000888 ) ;
#8821=EDGE_LOOP ( 'NONE', ( #3881, #2667, #4835, #8144 ) ) ;
#8824=ORIENTED_EDGE ( 'NONE', *, *, #6195, .T. ) ;
#8842=ORIENTED_EDGE ( 'NONE', *, *, #4128, .F. ) ;
#8860=CARTESIAN_POINT ( 'NONE',  ( 0.4129292217237342522, 28.50085334706577100, 1.500673695285823506 ) ) ;
#8862=EDGE_LOOP ( 'NONE', ( #4552, #5338, #5622, #1631 ) ) ;
#8864=FACE_OUTER_BOUND ( 'NONE', #9310, .T. ) ;
#8871=ORIENTED_EDGE ( 'NONE', *, *, #7669, .F. ) ;
#8902=ORIENTED_EDGE ( 'NONE', *, *, #7618, .F. ) ;
#8903=CARTESIAN_POINT ( 'NONE',  ( -0.2247925377428787452, 28.49955466461979015, 1.499648419317238357 ) ) ;
#8920=AXIS2_PLACEMENT_3D ( 'NONE', #5462, #8667, #8576 ) ;
#8932=DIRECTION ( 'NONE',  ( -1.000000000000000000, 0.000000000000000000, 0.000000000000000000 ) ) ;
#8936=CARTESIAN_POINT ( 'NONE',  ( 0.000000000000000000, 0.000000000000000000, 3.000000000000052847 ) ) ;
#8939=CARTESIAN_POINT ( 'NONE',  ( -22.50000000000000000, -7.855833012397050680E-14, 5.000000000000000000 ) ) ;
#8941=LINE ( 'NONE', #8762, #6501 ) ;
#8964=AXIS2_PLACEMENT_3D ( 'NONE', #3920, #6092, #1616 ) ;
#8969=AXIS2_PLACEMENT_3D ( 'NONE', #5319, #3918, #82 ) ;
#9007=CARTESIAN_POINT ( 'NONE',  ( -28.00000000000000711, 0.000000000000000000, 10.00000000000000000 ) ) ;
#9027=CARTESIAN_POINT ( 'NONE',  ( 26.91620486903881115, -4.078357040894570851, 0.2218373908656700588 ) ) ;
#9039=ORIENTED_EDGE ( 'NONE', *, *, #2300, .T. ) ;
#9047=ORIENTED_EDGE ( 'NONE', *, *, #7107, .T. ) ;
#9053=CARTESIAN_POINT ( 'NONE',  ( 0.000000000000000000, 22.50000000000000355, 5.000000000000000000 ) ) ;
#9068=ADVANCED_FACE ( 'NONE', ( #1774 ), #2552, .F. ) ;
#9076=DIRECTION ( 'NONE',  ( 1.000000000000000000, 0.000000000000000000, 0.000000000000000000 ) ) ;
#9098=AXIS2_PLACEMENT_3D ( 'NONE', #5322, #8250, #7523 ) ;
#9121=CARTESIAN_POINT ( 'NONE',  ( 1.571166602479410136E-13, -22.50000000000000355, 0.000000000000000000 ) ) ;
#9130=FACE_OUTER_BOUND ( 'NONE', #4162, .T. ) ;
#9138=DIRECTION ( 'NONE',  ( 1.000000000000000000, 0.000000000000000000, 0.000000000000000000 ) ) ;
#9153=ORIENTED_EDGE ( 'NONE', *, *, #1373, .F. ) ;
#9165=CIRCLE ( 'NONE', #5034, 6.000000000000001776 ) ;
#9198=DIRECTION ( 'NONE',  ( 1.000000000000000000, 1.776356839400250465E-15, 0.000000000000000000 ) ) ;
#9221=EDGE_CURVE ( 'NONE', #7742, #2498, #9165, .T. ) ;
#9233=EDGE_CURVE ( 'NONE', #5080, #6587, #2866, .T. ) ;
#9234=CARTESIAN_POINT ( 'NONE',  ( -27.16490240584776572, 3.793344078502526973, 0.4263419363949844110 ) ) ;
#9239=FACE_OUTER_BOUND ( 'NONE', #8590, .T. ) ;
#9255=AXIS2_PLACEMENT_3D ( 'NONE', #3538, #9294, #3440 ) ;
#9263=CIRCLE ( 'NONE', #8964, 15.00000000000000000 ) ;
#9269=DIRECTION ( 'NONE',  ( -0.000000000000000000, -0.000000000000000000, -1.000000000000000000 ) ) ;
#9279=DIRECTION ( 'NONE',  ( -0.000000000000000000, -0.000000000000000000, -1.000000000000000000 ) ) ;
#9289=EDGE_LOOP ( 'NONE', ( #4067, #4662 ) ) ;
#9293=CARTESIAN_POINT ( 'NONE',  ( 0.000000000000000000, 22.50000000000000355, 15.00000000000000000 ) ) ;
#9294=DIRECTION ( 'NONE',  ( 0.000000000000000000, 0.000000000000000000, -1.000000000000000000 ) ) ;
#9303=AXIS2_PLACEMENT_3D ( 'NONE', #7655, #4628, #5304 ) ;
#9306=CARTESIAN_POINT ( 'NONE',  ( 1.571166602479410136E-13, -22.50000000000000355, 15.00000000000000000 ) ) ;
#9310=EDGE_LOOP ( 'NONE', ( #7053, #7116, #2560, #9039, #7120, #3587 ) ) ;
#9313=VERTEX_POINT ( 'NONE', #6911 ) ;
#9325=ORIENTED_EDGE ( 'NONE', *, *, #6833, .T. ) ;
#9341=CARTESIAN_POINT ( 'NONE',  ( -2.081312099201802823, 28.14194242914269495, 1.216216932313278098 ) ) ;
#9348=ADVANCED_FACE ( 'NONE', ( #4880 ), #2773, .F. ) ;
#9353=EDGE_LOOP ( 'NONE', ( #7617, #2883, #3743, #6689 ) ) ;
#9367=AXIS2_PLACEMENT_3D ( 'NONE', #8495, #6336, #4840 ) ;
#9369=DIRECTION ( 'NONE',  ( -0.000000000000000000, -0.000000000000000000, -1.000000000000000000 ) ) ;
#9385=CARTESIAN_POINT ( 'NONE',  ( -2.060470863509831219, -28.13894063079882457, 1.213559982044000840 ) ) ;
#9391=CYLINDRICAL_SURFACE ( 'NONE', #1513, 15.00000000000000000 ) ;
#9394=DIRECTION ( 'NONE',  ( 1.000000000000000000, 0.000000000000000000, 0.000000000000000000 ) ) ;
#9400=VERTEX_POINT ( 'NONE', #1951 ) ;
#9407=LINE ( 'NONE', #5767, #2198 ) ;
#9413=VERTEX_POINT ( 'NONE', #3477 ) ;
#9419=EDGE_CURVE ( 'NONE', #4476, #410, #8180, .T. ) ;
#9437=CARTESIAN_POINT ( 'NONE',  ( -26.64999999999995950, -4.333301281932866900, 0.000000000000000000 ) ) ;
#9442=EDGE_CURVE ( 'NONE', #1701, #4799, #3624, .T. ) ;
#9445=ORIENTED_EDGE ( 'NONE', *, *, #6871, .F. ) ;
#9448=PRODUCT ( '5-Cover', '5-Cover', '', ( #3844 ) ) ;
#9457=EDGE_CURVE ( 'NONE', #1701, #8041, #6553, .T. ) ;
#9464=CIRCLE ( 'NONE', #1489, 6.000000000000001776 ) ;
#9469=DIRECTION ( 'NONE',  ( -1.000000000000000000, 0.000000000000000000, 0.000000000000000000 ) ) ;
#9516=COLOUR_RGB('Sky Blue',0.24,0.69,0.87);
#9517=FILL_AREA_STYLE_COLOUR('',#9516);
#9518=FILL_AREA_STYLE('',(#9517));
#9519=SURFACE_STYLE_FILL_AREA(#9518);
#9520=SURFACE_SIDE_STYLE('',(#9519));
#9521=SURFACE_STYLE_USAGE(.BOTH.,#9520);
#9522=PRESENTATION_STYLE_ASSIGNMENT((#9521));
ENDSEC;
END-ISO-10303-21;
